ISO-10303-21;
HEADER;
/* Generated by software containing ST-Developer
 * from STEP Tools, Inc. (www.steptools.com) 
 */

FILE_DESCRIPTION(
/* description */ ('STEP AP214'),
/* implementation_level */ '2;1');

FILE_NAME(
/* name */ 'Hex Finished Bolt 0.25-20x1.5x0.75-S.step',
/* time_stamp */ '2026-11-14T04:30:00-08:00',
/* author */ (''),
/* organization */ (''),
/* preprocessor_version */ 'ST-DEVELOPER v20.2',
/* originating_system */ 'Autodesk Translation Framework v15.17.0.0',
/* authorisation */ '');

FILE_SCHEMA (('AUTOMOTIVE_DESIGN { 1 0 10303 214 3 1 1 }'));
ENDSEC;

DATA;
#10=MECHANICAL_DESIGN_GEOMETRIC_PRESENTATION_REPRESENTATION('',(#128),#40809);
#112=SHAPE_REPRESENTATION_RELATIONSHIP('SRR','None',#40862,#120);
#120=ADVANCED_BREP_SHAPE_REPRESENTATION('',(#136),#40806);
#128=STYLED_ITEM('',(#40909),#136);
#136=MANIFOLD_SOLID_BREP('Body1',#6303);
#237=(
BOUNDED_CURVE()
B_SPLINE_CURVE(2,(#40369,#40370,#40371),.UNSPECIFIED.,.F.,.F.)
B_SPLINE_CURVE_WITH_KNOTS((3,3),(-1.35021080745884,-0.79564467090931),
 .UNSPECIFIED.)
CURVE()
GEOMETRIC_REPRESENTATION_ITEM()
RATIONAL_B_SPLINE_CURVE((1.74094633834734,1.74094633834734,1.61595201499016))
REPRESENTATION_ITEM('')
);
#238=(
BOUNDED_CURVE()
B_SPLINE_CURVE(2,(#40372,#40373,#40374),.UNSPECIFIED.,.F.,.F.)
B_SPLINE_CURVE_WITH_KNOTS((3,3),(-1.90477694400836,-1.35021080745884),
 .UNSPECIFIED.)
CURVE()
GEOMETRIC_REPRESENTATION_ITEM()
RATIONAL_B_SPLINE_CURVE((1.61595201499016,1.74094633834734,1.74094633834734))
REPRESENTATION_ITEM('')
);
#239=(
BOUNDED_CURVE()
B_SPLINE_CURVE(2,(#40377,#40378,#40379),.UNSPECIFIED.,.F.,.F.)
B_SPLINE_CURVE_WITH_KNOTS((3,3),(-1.35021080745884,-0.795644670909311),
 .UNSPECIFIED.)
CURVE()
GEOMETRIC_REPRESENTATION_ITEM()
RATIONAL_B_SPLINE_CURVE((1.74094633834734,1.74094633834734,1.61595201499016))
REPRESENTATION_ITEM('')
);
#240=(
BOUNDED_CURVE()
B_SPLINE_CURVE(2,(#40380,#40381,#40382),.UNSPECIFIED.,.F.,.F.)
B_SPLINE_CURVE_WITH_KNOTS((3,3),(-1.90477694400836,-1.35021080745884),
 .UNSPECIFIED.)
CURVE()
GEOMETRIC_REPRESENTATION_ITEM()
RATIONAL_B_SPLINE_CURVE((1.61595201499017,1.74094633834734,1.74094633834734))
REPRESENTATION_ITEM('')
);
#241=(
BOUNDED_CURVE()
B_SPLINE_CURVE(2,(#40385,#40386,#40387),.UNSPECIFIED.,.F.,.F.)
B_SPLINE_CURVE_WITH_KNOTS((3,3),(-1.90477694400836,-1.35021080745884),
 .UNSPECIFIED.)
CURVE()
GEOMETRIC_REPRESENTATION_ITEM()
RATIONAL_B_SPLINE_CURVE((1.61595201499017,1.74094633834734,1.74094633834734))
REPRESENTATION_ITEM('')
);
#242=(
BOUNDED_CURVE()
B_SPLINE_CURVE(2,(#40388,#40389,#40390),.UNSPECIFIED.,.F.,.F.)
B_SPLINE_CURVE_WITH_KNOTS((3,3),(-1.35021080745884,-0.795644670909311),
 .UNSPECIFIED.)
CURVE()
GEOMETRIC_REPRESENTATION_ITEM()
RATIONAL_B_SPLINE_CURVE((1.74094633834735,1.74094633834735,1.61595201499017))
REPRESENTATION_ITEM('')
);
#243=(
BOUNDED_CURVE()
B_SPLINE_CURVE(2,(#40393,#40394,#40395),.UNSPECIFIED.,.F.,.F.)
B_SPLINE_CURVE_WITH_KNOTS((3,3),(-1.90477694400837,-1.35021080745884),
 .UNSPECIFIED.)
CURVE()
GEOMETRIC_REPRESENTATION_ITEM()
RATIONAL_B_SPLINE_CURVE((1.61595201499017,1.74094633834735,1.74094633834735))
REPRESENTATION_ITEM('')
);
#244=(
BOUNDED_CURVE()
B_SPLINE_CURVE(2,(#40396,#40397,#40398),.UNSPECIFIED.,.F.,.F.)
B_SPLINE_CURVE_WITH_KNOTS((3,3),(-1.35021080745884,-0.795644670909312),
 .UNSPECIFIED.)
CURVE()
GEOMETRIC_REPRESENTATION_ITEM()
RATIONAL_B_SPLINE_CURVE((1.74094633834734,1.74094633834734,1.61595201499016))
REPRESENTATION_ITEM('')
);
#245=(
BOUNDED_CURVE()
B_SPLINE_CURVE(2,(#40401,#40402,#40403),.UNSPECIFIED.,.F.,.F.)
B_SPLINE_CURVE_WITH_KNOTS((3,3),(-1.35021080745884,-0.795644670909311),
 .UNSPECIFIED.)
CURVE()
GEOMETRIC_REPRESENTATION_ITEM()
RATIONAL_B_SPLINE_CURVE((1.74094633834734,1.74094633834734,1.61595201499016))
REPRESENTATION_ITEM('')
);
#246=(
BOUNDED_CURVE()
B_SPLINE_CURVE(2,(#40404,#40405,#40406),.UNSPECIFIED.,.F.,.F.)
B_SPLINE_CURVE_WITH_KNOTS((3,3),(-1.90477694400836,-1.35021080745884),
 .UNSPECIFIED.)
CURVE()
GEOMETRIC_REPRESENTATION_ITEM()
RATIONAL_B_SPLINE_CURVE((1.61595201499016,1.74094633834734,1.74094633834734))
REPRESENTATION_ITEM('')
);
#247=(
BOUNDED_CURVE()
B_SPLINE_CURVE(2,(#40409,#40410,#40411),.UNSPECIFIED.,.F.,.F.)
B_SPLINE_CURVE_WITH_KNOTS((3,3),(-1.90477694400833,-1.35021080745884),
 .UNSPECIFIED.)
CURVE()
GEOMETRIC_REPRESENTATION_ITEM()
RATIONAL_B_SPLINE_CURVE((1.61595201499018,1.74094633834734,1.74094633834734))
REPRESENTATION_ITEM('')
);
#248=(
BOUNDED_CURVE()
B_SPLINE_CURVE(2,(#40412,#40413,#40414),.UNSPECIFIED.,.F.,.F.)
B_SPLINE_CURVE_WITH_KNOTS((3,3),(-1.35021080745884,-0.795644670909275),
 .UNSPECIFIED.)
CURVE()
GEOMETRIC_REPRESENTATION_ITEM()
RATIONAL_B_SPLINE_CURVE((1.74094633834734,1.74094633834734,1.61595201499015))
REPRESENTATION_ITEM('')
);
#298=PLANE('',#6987);
#299=PLANE('',#6988);
#300=PLANE('',#6989);
#301=PLANE('',#6990);
#302=PLANE('',#6991);
#303=PLANE('',#6992);
#304=PLANE('',#6993);
#305=PLANE('',#6994);
#306=PLANE('',#7007);
#307=PLANE('',#7008);
#308=PLANE('',#7009);
#309=PLANE('',#7010);
#310=PLANE('',#7011);
#311=PLANE('',#7012);
#312=PLANE('',#7013);
#354=FACE_BOUND('',#1197,.T.);
#407=CONICAL_SURFACE('',#6837,2.41935,0.785398163397442);
#408=CONICAL_SURFACE('',#6841,2.41935,0.959931088596876);
#409=CONICAL_SURFACE('',#6846,3.175,0.959931088596883);
#410=CONICAL_SURFACE('',#6850,2.41935,0.959931088596876);
#411=CONICAL_SURFACE('',#6855,3.175,0.959931088596883);
#412=CONICAL_SURFACE('',#6859,2.41935,0.959931088596876);
#413=CONICAL_SURFACE('',#6864,3.175,0.959931088596883);
#414=CONICAL_SURFACE('',#6868,2.41935,0.959931088596876);
#415=CONICAL_SURFACE('',#6873,3.175,0.959931088596883);
#416=CONICAL_SURFACE('',#6877,2.41935,0.959931088596876);
#417=CONICAL_SURFACE('',#6882,3.175,0.959931088596883);
#418=CONICAL_SURFACE('',#6886,2.41935,0.959931088596876);
#419=CONICAL_SURFACE('',#6891,3.175,0.959931088596883);
#420=CONICAL_SURFACE('',#6895,2.41935,0.959931088596876);
#421=CONICAL_SURFACE('',#6900,3.175,0.959931088596883);
#422=CONICAL_SURFACE('',#6904,2.41935,0.959931088596876);
#423=CONICAL_SURFACE('',#6909,3.175,0.959931088596883);
#424=CONICAL_SURFACE('',#6913,2.41935,0.959931088596876);
#425=CONICAL_SURFACE('',#6918,3.175,0.959931088596883);
#426=CONICAL_SURFACE('',#6922,2.41935,0.959931088596876);
#427=CONICAL_SURFACE('',#6927,3.175,0.959931088596883);
#428=CONICAL_SURFACE('',#6931,2.41935,0.959931088596876);
#429=CONICAL_SURFACE('',#6936,3.175,0.959931088596883);
#430=CONICAL_SURFACE('',#6940,2.41935,0.959931088596876);
#431=CONICAL_SURFACE('',#6945,3.175,0.959931088596883);
#432=CONICAL_SURFACE('',#6949,2.41935,0.959931088596876);
#433=CONICAL_SURFACE('',#6954,3.175,0.959931088596883);
#434=CONICAL_SURFACE('',#6958,2.41935,0.959931088596876);
#435=CONICAL_SURFACE('',#6963,3.175,0.959931088596883);
#436=CONICAL_SURFACE('',#6967,2.41935,0.959931088596876);
#437=CONICAL_SURFACE('',#6972,3.175,0.959931088596883);
#438=CONICAL_SURFACE('',#7001,5.5626,1.0471975511966);
#439=CONICAL_SURFACE('',#7002,5.5626,1.0471975511966);
#440=CONICAL_SURFACE('',#7003,5.5626,1.0471975511966);
#441=CONICAL_SURFACE('',#7004,5.5626,1.0471975511966);
#442=CONICAL_SURFACE('',#7005,5.5626,1.0471975511966);
#443=CONICAL_SURFACE('',#7006,5.5626,1.0471975511966);
#489=TOROIDAL_SURFACE('',#6973,3.556,0.381);
#746=FACE_OUTER_BOUND('',#1148,.T.);
#747=FACE_OUTER_BOUND('',#1149,.T.);
#748=FACE_OUTER_BOUND('',#1150,.T.);
#749=FACE_OUTER_BOUND('',#1151,.T.);
#750=FACE_OUTER_BOUND('',#1152,.T.);
#751=FACE_OUTER_BOUND('',#1153,.T.);
#752=FACE_OUTER_BOUND('',#1154,.T.);
#753=FACE_OUTER_BOUND('',#1155,.T.);
#754=FACE_OUTER_BOUND('',#1156,.T.);
#755=FACE_OUTER_BOUND('',#1157,.T.);
#756=FACE_OUTER_BOUND('',#1158,.T.);
#757=FACE_OUTER_BOUND('',#1159,.T.);
#758=FACE_OUTER_BOUND('',#1160,.T.);
#759=FACE_OUTER_BOUND('',#1161,.T.);
#760=FACE_OUTER_BOUND('',#1162,.T.);
#761=FACE_OUTER_BOUND('',#1163,.T.);
#762=FACE_OUTER_BOUND('',#1164,.T.);
#763=FACE_OUTER_BOUND('',#1165,.T.);
#764=FACE_OUTER_BOUND('',#1166,.T.);
#765=FACE_OUTER_BOUND('',#1167,.T.);
#766=FACE_OUTER_BOUND('',#1168,.T.);
#767=FACE_OUTER_BOUND('',#1169,.T.);
#768=FACE_OUTER_BOUND('',#1170,.T.);
#769=FACE_OUTER_BOUND('',#1171,.T.);
#770=FACE_OUTER_BOUND('',#1172,.T.);
#771=FACE_OUTER_BOUND('',#1173,.T.);
#772=FACE_OUTER_BOUND('',#1174,.T.);
#773=FACE_OUTER_BOUND('',#1175,.T.);
#774=FACE_OUTER_BOUND('',#1176,.T.);
#775=FACE_OUTER_BOUND('',#1177,.T.);
#776=FACE_OUTER_BOUND('',#1178,.T.);
#777=FACE_OUTER_BOUND('',#1179,.T.);
#778=FACE_OUTER_BOUND('',#1180,.T.);
#779=FACE_OUTER_BOUND('',#1181,.T.);
#780=FACE_OUTER_BOUND('',#1182,.T.);
#781=FACE_OUTER_BOUND('',#1183,.T.);
#782=FACE_OUTER_BOUND('',#1184,.T.);
#783=FACE_OUTER_BOUND('',#1185,.T.);
#784=FACE_OUTER_BOUND('',#1186,.T.);
#785=FACE_OUTER_BOUND('',#1187,.T.);
#786=FACE_OUTER_BOUND('',#1188,.T.);
#787=FACE_OUTER_BOUND('',#1189,.T.);
#788=FACE_OUTER_BOUND('',#1190,.T.);
#789=FACE_OUTER_BOUND('',#1191,.T.);
#790=FACE_OUTER_BOUND('',#1192,.T.);
#791=FACE_OUTER_BOUND('',#1193,.T.);
#792=FACE_OUTER_BOUND('',#1194,.T.);
#793=FACE_OUTER_BOUND('',#1195,.T.);
#794=FACE_OUTER_BOUND('',#1196,.T.);
#795=FACE_OUTER_BOUND('',#1198,.T.);
#796=FACE_OUTER_BOUND('',#1199,.T.);
#797=FACE_OUTER_BOUND('',#1200,.T.);
#798=FACE_OUTER_BOUND('',#1201,.T.);
#799=FACE_OUTER_BOUND('',#1202,.T.);
#800=FACE_OUTER_BOUND('',#1203,.T.);
#801=FACE_OUTER_BOUND('',#1204,.T.);
#802=FACE_OUTER_BOUND('',#1205,.T.);
#803=FACE_OUTER_BOUND('',#1206,.T.);
#804=FACE_OUTER_BOUND('',#1207,.T.);
#805=FACE_OUTER_BOUND('',#1208,.T.);
#806=FACE_OUTER_BOUND('',#1209,.T.);
#807=FACE_OUTER_BOUND('',#1210,.T.);
#808=FACE_OUTER_BOUND('',#1211,.T.);
#809=FACE_OUTER_BOUND('',#1212,.T.);
#810=FACE_OUTER_BOUND('',#1213,.T.);
#811=FACE_OUTER_BOUND('',#1214,.T.);
#812=FACE_OUTER_BOUND('',#1215,.T.);
#813=FACE_OUTER_BOUND('',#1216,.T.);
#814=FACE_OUTER_BOUND('',#1217,.T.);
#1148=EDGE_LOOP('',(#5108,#5109,#5110,#5111,#5112));
#1149=EDGE_LOOP('',(#5113,#5114,#5115,#5116,#5117,#5118));
#1150=EDGE_LOOP('',(#5119,#5120,#5121,#5122,#5123,#5124));
#1151=EDGE_LOOP('',(#5125,#5126,#5127,#5128,#5129,#5130));
#1152=EDGE_LOOP('',(#5131,#5132,#5133,#5134,#5135,#5136));
#1153=EDGE_LOOP('',(#5137,#5138,#5139,#5140,#5141,#5142));
#1154=EDGE_LOOP('',(#5143,#5144,#5145,#5146,#5147,#5148));
#1155=EDGE_LOOP('',(#5149,#5150,#5151,#5152,#5153,#5154));
#1156=EDGE_LOOP('',(#5155,#5156,#5157,#5158,#5159,#5160));
#1157=EDGE_LOOP('',(#5161,#5162,#5163,#5164,#5165,#5166));
#1158=EDGE_LOOP('',(#5167,#5168,#5169,#5170,#5171,#5172));
#1159=EDGE_LOOP('',(#5173,#5174,#5175,#5176,#5177,#5178));
#1160=EDGE_LOOP('',(#5179,#5180,#5181,#5182,#5183,#5184));
#1161=EDGE_LOOP('',(#5185,#5186,#5187,#5188,#5189,#5190));
#1162=EDGE_LOOP('',(#5191,#5192,#5193,#5194,#5195,#5196));
#1163=EDGE_LOOP('',(#5197,#5198,#5199,#5200,#5201,#5202));
#1164=EDGE_LOOP('',(#5203,#5204,#5205,#5206,#5207,#5208));
#1165=EDGE_LOOP('',(#5209,#5210,#5211,#5212,#5213,#5214));
#1166=EDGE_LOOP('',(#5215,#5216,#5217,#5218,#5219,#5220));
#1167=EDGE_LOOP('',(#5221,#5222,#5223,#5224,#5225,#5226));
#1168=EDGE_LOOP('',(#5227,#5228,#5229,#5230,#5231,#5232));
#1169=EDGE_LOOP('',(#5233,#5234,#5235,#5236,#5237,#5238));
#1170=EDGE_LOOP('',(#5239,#5240,#5241,#5242,#5243,#5244));
#1171=EDGE_LOOP('',(#5245,#5246,#5247,#5248,#5249,#5250));
#1172=EDGE_LOOP('',(#5251,#5252,#5253,#5254,#5255,#5256));
#1173=EDGE_LOOP('',(#5257,#5258,#5259,#5260,#5261,#5262));
#1174=EDGE_LOOP('',(#5263,#5264,#5265,#5266,#5267,#5268));
#1175=EDGE_LOOP('',(#5269,#5270,#5271,#5272,#5273,#5274));
#1176=EDGE_LOOP('',(#5275,#5276,#5277,#5278,#5279,#5280));
#1177=EDGE_LOOP('',(#5281,#5282,#5283,#5284,#5285,#5286));
#1178=EDGE_LOOP('',(#5287,#5288,#5289,#5290,#5291,#5292));
#1179=EDGE_LOOP('',(#5293,#5294,#5295,#5296,#5297,#5298));
#1180=EDGE_LOOP('',(#5299,#5300,#5301,#5302,#5303,#5304));
#1181=EDGE_LOOP('',(#5305,#5306,#5307,#5308,#5309,#5310));
#1182=EDGE_LOOP('',(#5311,#5312,#5313,#5314,#5315,#5316));
#1183=EDGE_LOOP('',(#5317,#5318,#5319,#5320,#5321,#5322));
#1184=EDGE_LOOP('',(#5323,#5324,#5325,#5326,#5327,#5328));
#1185=EDGE_LOOP('',(#5329,#5330,#5331,#5332,#5333,#5334));
#1186=EDGE_LOOP('',(#5335,#5336,#5337,#5338,#5339,#5340));
#1187=EDGE_LOOP('',(#5341,#5342,#5343,#5344,#5345,#5346));
#1188=EDGE_LOOP('',(#5347,#5348,#5349,#5350,#5351,#5352));
#1189=EDGE_LOOP('',(#5353,#5354,#5355,#5356,#5357,#5358));
#1190=EDGE_LOOP('',(#5359,#5360,#5361,#5362,#5363,#5364));
#1191=EDGE_LOOP('',(#5365,#5366,#5367,#5368,#5369,#5370));
#1192=EDGE_LOOP('',(#5371,#5372,#5373,#5374,#5375,#5376));
#1193=EDGE_LOOP('',(#5377,#5378,#5379,#5380,#5381));
#1194=EDGE_LOOP('',(#5382,#5383,#5384,#5385,#5386,#5387,#5388,#5389,#5390));
#1195=EDGE_LOOP('',(#5391,#5392,#5393,#5394,#5395,#5396));
#1196=EDGE_LOOP('',(#5397));
#1197=EDGE_LOOP('',(#5398));
#1198=EDGE_LOOP('',(#5399,#5400,#5401));
#1199=EDGE_LOOP('',(#5402,#5403,#5404));
#1200=EDGE_LOOP('',(#5405,#5406,#5407));
#1201=EDGE_LOOP('',(#5408,#5409,#5410));
#1202=EDGE_LOOP('',(#5411,#5412,#5413));
#1203=EDGE_LOOP('',(#5414,#5415,#5416));
#1204=EDGE_LOOP('',(#5417,#5418,#5419,#5420,#5421,#5422));
#1205=EDGE_LOOP('',(#5423,#5424,#5425));
#1206=EDGE_LOOP('',(#5426,#5427,#5428));
#1207=EDGE_LOOP('',(#5429,#5430,#5431));
#1208=EDGE_LOOP('',(#5432,#5433,#5434));
#1209=EDGE_LOOP('',(#5435,#5436,#5437));
#1210=EDGE_LOOP('',(#5438,#5439,#5440));
#1211=EDGE_LOOP('',(#5441,#5442,#5443,#5444,#5445,#5446));
#1212=EDGE_LOOP('',(#5447,#5448,#5449,#5450,#5451,#5452));
#1213=EDGE_LOOP('',(#5453,#5454,#5455,#5456,#5457,#5458));
#1214=EDGE_LOOP('',(#5459,#5460,#5461,#5462,#5463,#5464));
#1215=EDGE_LOOP('',(#5465,#5466,#5467,#5468,#5469,#5470));
#1216=EDGE_LOOP('',(#5471,#5472,#5473,#5474,#5475,#5476));
#1217=EDGE_LOOP('',(#5477));
#1515=CIRCLE('',#6838,3.16631763274988);
#1516=CIRCLE('',#6839,3.16631763274988);
#1517=CIRCLE('',#6840,2.41935);
#1518=CIRCLE('',#6842,3.175);
#1519=CIRCLE('',#6843,3.175);
#1520=CIRCLE('',#6844,2.41935);
#1521=CIRCLE('',#6845,2.41935);
#1522=CIRCLE('',#6848,3.175);
#1523=CIRCLE('',#6849,3.175);
#1524=CIRCLE('',#6851,3.175);
#1525=CIRCLE('',#6852,3.175);
#1526=CIRCLE('',#6853,2.41935);
#1527=CIRCLE('',#6854,2.41935);
#1528=CIRCLE('',#6857,3.175);
#1529=CIRCLE('',#6858,3.175);
#1530=CIRCLE('',#6860,3.175);
#1531=CIRCLE('',#6861,3.175);
#1532=CIRCLE('',#6862,2.41935);
#1533=CIRCLE('',#6863,2.41935);
#1534=CIRCLE('',#6866,3.175);
#1535=CIRCLE('',#6867,3.175);
#1536=CIRCLE('',#6869,3.175);
#1537=CIRCLE('',#6870,3.175);
#1538=CIRCLE('',#6871,2.41935);
#1539=CIRCLE('',#6872,2.41935);
#1540=CIRCLE('',#6875,3.175);
#1541=CIRCLE('',#6876,3.175);
#1542=CIRCLE('',#6878,3.175);
#1543=CIRCLE('',#6879,3.175);
#1544=CIRCLE('',#6880,2.41935);
#1545=CIRCLE('',#6881,2.41935);
#1546=CIRCLE('',#6884,3.175);
#1547=CIRCLE('',#6885,3.175);
#1548=CIRCLE('',#6887,3.175);
#1549=CIRCLE('',#6888,3.175);
#1550=CIRCLE('',#6889,2.41935);
#1551=CIRCLE('',#6890,2.41935);
#1552=CIRCLE('',#6893,3.175);
#1553=CIRCLE('',#6894,3.175);
#1554=CIRCLE('',#6896,3.175);
#1555=CIRCLE('',#6897,3.175);
#1556=CIRCLE('',#6898,2.41935);
#1557=CIRCLE('',#6899,2.41935);
#1558=CIRCLE('',#6902,3.175);
#1559=CIRCLE('',#6903,3.175);
#1560=CIRCLE('',#6905,3.175);
#1561=CIRCLE('',#6906,3.175);
#1562=CIRCLE('',#6907,2.41935);
#1563=CIRCLE('',#6908,2.41935);
#1564=CIRCLE('',#6911,3.175);
#1565=CIRCLE('',#6912,3.175);
#1566=CIRCLE('',#6914,3.175);
#1567=CIRCLE('',#6915,3.175);
#1568=CIRCLE('',#6916,2.41935);
#1569=CIRCLE('',#6917,2.41935);
#1570=CIRCLE('',#6920,3.175);
#1571=CIRCLE('',#6921,3.175);
#1572=CIRCLE('',#6923,3.175);
#1573=CIRCLE('',#6924,3.175);
#1574=CIRCLE('',#6925,2.41935);
#1575=CIRCLE('',#6926,2.41935);
#1576=CIRCLE('',#6929,3.175);
#1577=CIRCLE('',#6930,3.175);
#1578=CIRCLE('',#6932,3.175);
#1579=CIRCLE('',#6933,3.175);
#1580=CIRCLE('',#6934,2.41935);
#1581=CIRCLE('',#6935,2.41935);
#1582=CIRCLE('',#6938,3.175);
#1583=CIRCLE('',#6939,3.175);
#1584=CIRCLE('',#6941,3.175);
#1585=CIRCLE('',#6942,3.175);
#1586=CIRCLE('',#6943,2.41935);
#1587=CIRCLE('',#6944,2.41935);
#1588=CIRCLE('',#6947,3.175);
#1589=CIRCLE('',#6948,3.175);
#1590=CIRCLE('',#6950,3.175);
#1591=CIRCLE('',#6951,3.175);
#1592=CIRCLE('',#6952,2.41935);
#1593=CIRCLE('',#6953,2.41935);
#1594=CIRCLE('',#6956,3.175);
#1595=CIRCLE('',#6957,3.175);
#1596=CIRCLE('',#6959,3.175);
#1597=CIRCLE('',#6960,3.175);
#1598=CIRCLE('',#6961,2.41935);
#1599=CIRCLE('',#6962,2.41935);
#1600=CIRCLE('',#6965,3.175);
#1601=CIRCLE('',#6966,3.175);
#1602=CIRCLE('',#6968,3.175);
#1603=CIRCLE('',#6969,3.175);
#1604=CIRCLE('',#6970,2.41935);
#1605=CIRCLE('',#6971,2.41935);
#1606=CIRCLE('',#6974,3.175);
#1607=CIRCLE('',#6975,3.175);
#1608=CIRCLE('',#6976,0.381);
#1609=CIRCLE('',#6977,3.556);
#1610=CIRCLE('',#6979,5.5626);
#1611=CIRCLE('',#6980,5.5626);
#1612=CIRCLE('',#6981,5.5626);
#1613=CIRCLE('',#6982,5.5626);
#1614=CIRCLE('',#6983,5.5626);
#1615=CIRCLE('',#6984,5.5626);
#1616=CIRCLE('',#6985,5.5626);
#1617=CIRCLE('',#6995,5.5626);
#1618=CIRCLE('',#6996,5.5626);
#1619=CIRCLE('',#6997,5.5626);
#1620=CIRCLE('',#6998,5.5626);
#1621=CIRCLE('',#6999,5.5626);
#1622=CIRCLE('',#7000,5.5626);
#2006=LINE('',#40037,#2324);
#2007=LINE('',#40045,#2325);
#2008=LINE('',#40050,#2326);
#2009=LINE('',#40056,#2327);
#2010=LINE('',#40063,#2328);
#2011=LINE('',#40068,#2329);
#2012=LINE('',#40074,#2330);
#2013=LINE('',#40081,#2331);
#2014=LINE('',#40086,#2332);
#2015=LINE('',#40092,#2333);
#2016=LINE('',#40099,#2334);
#2017=LINE('',#40104,#2335);
#2018=LINE('',#40110,#2336);
#2019=LINE('',#40117,#2337);
#2020=LINE('',#40122,#2338);
#2021=LINE('',#40128,#2339);
#2022=LINE('',#40135,#2340);
#2023=LINE('',#40140,#2341);
#2024=LINE('',#40146,#2342);
#2025=LINE('',#40153,#2343);
#2026=LINE('',#40158,#2344);
#2027=LINE('',#40164,#2345);
#2028=LINE('',#40171,#2346);
#2029=LINE('',#40176,#2347);
#2030=LINE('',#40182,#2348);
#2031=LINE('',#40189,#2349);
#2032=LINE('',#40194,#2350);
#2033=LINE('',#40200,#2351);
#2034=LINE('',#40207,#2352);
#2035=LINE('',#40212,#2353);
#2036=LINE('',#40218,#2354);
#2037=LINE('',#40225,#2355);
#2038=LINE('',#40230,#2356);
#2039=LINE('',#40236,#2357);
#2040=LINE('',#40243,#2358);
#2041=LINE('',#40248,#2359);
#2042=LINE('',#40254,#2360);
#2043=LINE('',#40261,#2361);
#2044=LINE('',#40266,#2362);
#2045=LINE('',#40272,#2363);
#2046=LINE('',#40279,#2364);
#2047=LINE('',#40284,#2365);
#2048=LINE('',#40290,#2366);
#2049=LINE('',#40297,#2367);
#2050=LINE('',#40302,#2368);
#2051=LINE('',#40320,#2369);
#2052=LINE('',#40328,#2370);
#2053=LINE('',#40332,#2371);
#2054=LINE('',#40333,#2372);
#2055=LINE('',#40336,#2373);
#2056=LINE('',#40337,#2374);
#2057=LINE('',#40340,#2375);
#2058=LINE('',#40341,#2376);
#2059=LINE('',#40344,#2377);
#2060=LINE('',#40345,#2378);
#2061=LINE('',#40348,#2379);
#2062=LINE('',#40349,#2380);
#2063=LINE('',#40352,#2381);
#2064=LINE('',#40353,#2382);
#2065=LINE('',#40416,#2383);
#2066=LINE('',#40417,#2384);
#2067=LINE('',#40419,#2385);
#2068=LINE('',#40421,#2386);
#2069=LINE('',#40423,#2387);
#2070=LINE('',#40425,#2388);
#2324=VECTOR('',#8254,2.41935);
#2325=VECTOR('',#8263,2.41935);
#2326=VECTOR('',#8270,3.175);
#2327=VECTOR('',#8277,3.175);
#2328=VECTOR('',#8284,2.41935);
#2329=VECTOR('',#8291,3.175);
#2330=VECTOR('',#8298,3.175);
#2331=VECTOR('',#8305,2.41935);
#2332=VECTOR('',#8312,3.175);
#2333=VECTOR('',#8319,3.175);
#2334=VECTOR('',#8326,2.41935);
#2335=VECTOR('',#8333,3.175);
#2336=VECTOR('',#8340,3.175);
#2337=VECTOR('',#8347,2.41935);
#2338=VECTOR('',#8354,3.175);
#2339=VECTOR('',#8361,3.175);
#2340=VECTOR('',#8368,2.41935);
#2341=VECTOR('',#8375,3.175);
#2342=VECTOR('',#8382,3.175);
#2343=VECTOR('',#8389,2.41935);
#2344=VECTOR('',#8396,3.175);
#2345=VECTOR('',#8403,3.175);
#2346=VECTOR('',#8410,2.41935);
#2347=VECTOR('',#8417,3.175);
#2348=VECTOR('',#8424,3.175);
#2349=VECTOR('',#8431,2.41935);
#2350=VECTOR('',#8438,3.175);
#2351=VECTOR('',#8445,3.175);
#2352=VECTOR('',#8452,2.41935);
#2353=VECTOR('',#8459,3.175);
#2354=VECTOR('',#8466,3.175);
#2355=VECTOR('',#8473,2.41935);
#2356=VECTOR('',#8480,3.175);
#2357=VECTOR('',#8487,3.175);
#2358=VECTOR('',#8494,2.41935);
#2359=VECTOR('',#8501,3.175);
#2360=VECTOR('',#8508,3.175);
#2361=VECTOR('',#8515,2.41935);
#2362=VECTOR('',#8522,3.175);
#2363=VECTOR('',#8529,3.175);
#2364=VECTOR('',#8536,2.41935);
#2365=VECTOR('',#8543,3.175);
#2366=VECTOR('',#8550,3.175);
#2367=VECTOR('',#8557,2.41935);
#2368=VECTOR('',#8564,3.175);
#2369=VECTOR('',#8583,5.5626);
#2370=VECTOR('',#8594,3.175);
#2371=VECTOR('',#8599,1000.);
#2372=VECTOR('',#8600,1000.);
#2373=VECTOR('',#8603,1000.);
#2374=VECTOR('',#8604,1000.);
#2375=VECTOR('',#8607,1000.);
#2376=VECTOR('',#8608,1000.);
#2377=VECTOR('',#8611,1000.);
#2378=VECTOR('',#8612,1000.);
#2379=VECTOR('',#8615,1000.);
#2380=VECTOR('',#8616,1000.);
#2381=VECTOR('',#8619,1000.);
#2382=VECTOR('',#8620,1000.);
#2383=VECTOR('',#8649,1000.);
#2384=VECTOR('',#8650,1000.);
#2385=VECTOR('',#8653,1000.);
#2386=VECTOR('',#8656,1000.);
#2387=VECTOR('',#8659,1000.);
#2388=VECTOR('',#8662,1000.);
#2816=VERTEX_POINT('',#40032);
#2817=VERTEX_POINT('',#40033);
#2818=VERTEX_POINT('',#40036);
#2819=VERTEX_POINT('',#40040);
#2820=VERTEX_POINT('',#40041);
#2821=VERTEX_POINT('',#40044);
#2822=VERTEX_POINT('',#40046);
#2823=VERTEX_POINT('',#40052);
#2824=VERTEX_POINT('',#40053);
#2825=VERTEX_POINT('',#40058);
#2826=VERTEX_POINT('',#40059);
#2827=VERTEX_POINT('',#40062);
#2828=VERTEX_POINT('',#40064);
#2829=VERTEX_POINT('',#40070);
#2830=VERTEX_POINT('',#40071);
#2831=VERTEX_POINT('',#40076);
#2832=VERTEX_POINT('',#40077);
#2833=VERTEX_POINT('',#40080);
#2834=VERTEX_POINT('',#40082);
#2835=VERTEX_POINT('',#40088);
#2836=VERTEX_POINT('',#40089);
#2837=VERTEX_POINT('',#40094);
#2838=VERTEX_POINT('',#40095);
#2839=VERTEX_POINT('',#40098);
#2840=VERTEX_POINT('',#40100);
#2841=VERTEX_POINT('',#40106);
#2842=VERTEX_POINT('',#40107);
#2843=VERTEX_POINT('',#40112);
#2844=VERTEX_POINT('',#40113);
#2845=VERTEX_POINT('',#40116);
#2846=VERTEX_POINT('',#40118);
#2847=VERTEX_POINT('',#40124);
#2848=VERTEX_POINT('',#40125);
#2849=VERTEX_POINT('',#40130);
#2850=VERTEX_POINT('',#40131);
#2851=VERTEX_POINT('',#40134);
#2852=VERTEX_POINT('',#40136);
#2853=VERTEX_POINT('',#40142);
#2854=VERTEX_POINT('',#40143);
#2855=VERTEX_POINT('',#40148);
#2856=VERTEX_POINT('',#40149);
#2857=VERTEX_POINT('',#40152);
#2858=VERTEX_POINT('',#40154);
#2859=VERTEX_POINT('',#40160);
#2860=VERTEX_POINT('',#40161);
#2861=VERTEX_POINT('',#40166);
#2862=VERTEX_POINT('',#40167);
#2863=VERTEX_POINT('',#40170);
#2864=VERTEX_POINT('',#40172);
#2865=VERTEX_POINT('',#40178);
#2866=VERTEX_POINT('',#40179);
#2867=VERTEX_POINT('',#40184);
#2868=VERTEX_POINT('',#40185);
#2869=VERTEX_POINT('',#40188);
#2870=VERTEX_POINT('',#40190);
#2871=VERTEX_POINT('',#40196);
#2872=VERTEX_POINT('',#40197);
#2873=VERTEX_POINT('',#40202);
#2874=VERTEX_POINT('',#40203);
#2875=VERTEX_POINT('',#40206);
#2876=VERTEX_POINT('',#40208);
#2877=VERTEX_POINT('',#40214);
#2878=VERTEX_POINT('',#40215);
#2879=VERTEX_POINT('',#40220);
#2880=VERTEX_POINT('',#40221);
#2881=VERTEX_POINT('',#40224);
#2882=VERTEX_POINT('',#40226);
#2883=VERTEX_POINT('',#40232);
#2884=VERTEX_POINT('',#40233);
#2885=VERTEX_POINT('',#40238);
#2886=VERTEX_POINT('',#40239);
#2887=VERTEX_POINT('',#40242);
#2888=VERTEX_POINT('',#40244);
#2889=VERTEX_POINT('',#40250);
#2890=VERTEX_POINT('',#40251);
#2891=VERTEX_POINT('',#40256);
#2892=VERTEX_POINT('',#40257);
#2893=VERTEX_POINT('',#40260);
#2894=VERTEX_POINT('',#40262);
#2895=VERTEX_POINT('',#40268);
#2896=VERTEX_POINT('',#40269);
#2897=VERTEX_POINT('',#40274);
#2898=VERTEX_POINT('',#40275);
#2899=VERTEX_POINT('',#40278);
#2900=VERTEX_POINT('',#40280);
#2901=VERTEX_POINT('',#40286);
#2902=VERTEX_POINT('',#40287);
#2903=VERTEX_POINT('',#40292);
#2904=VERTEX_POINT('',#40293);
#2905=VERTEX_POINT('',#40296);
#2906=VERTEX_POINT('',#40298);
#2907=VERTEX_POINT('',#40304);
#2908=VERTEX_POINT('',#40305);
#2909=VERTEX_POINT('',#40308);
#2910=VERTEX_POINT('',#40312);
#2911=VERTEX_POINT('',#40313);
#2912=VERTEX_POINT('',#40315);
#2913=VERTEX_POINT('',#40317);
#2914=VERTEX_POINT('',#40319);
#2915=VERTEX_POINT('',#40322);
#2916=VERTEX_POINT('',#40324);
#2917=VERTEX_POINT('',#40331);
#2918=VERTEX_POINT('',#40335);
#2919=VERTEX_POINT('',#40339);
#2920=VERTEX_POINT('',#40343);
#2921=VERTEX_POINT('',#40347);
#2922=VERTEX_POINT('',#40351);
#2923=VERTEX_POINT('',#40355);
#2924=VERTEX_POINT('',#40356);
#2925=VERTEX_POINT('',#40358);
#2926=VERTEX_POINT('',#40360);
#2927=VERTEX_POINT('',#40362);
#2928=VERTEX_POINT('',#40364);
#2929=VERTEX_POINT('',#40368);
#2930=VERTEX_POINT('',#40376);
#2931=VERTEX_POINT('',#40384);
#2932=VERTEX_POINT('',#40392);
#2933=VERTEX_POINT('',#40400);
#2934=VERTEX_POINT('',#40408);
#3606=EDGE_CURVE('',#2816,#2817,#1515,.T.);
#3607=EDGE_CURVE('',#2817,#2816,#1516,.T.);
#3608=EDGE_CURVE('',#2816,#2818,#2006,.T.);
#3609=EDGE_CURVE('',#2818,#2818,#1517,.T.);
#3610=EDGE_CURVE('',#2819,#2820,#1518,.T.);
#3611=EDGE_CURVE('',#2820,#2819,#1519,.T.);
#3612=EDGE_CURVE('',#2820,#2821,#2007,.T.);
#3613=EDGE_CURVE('',#2821,#2822,#1520,.T.);
#3614=EDGE_CURVE('',#2822,#2821,#1521,.T.);
#3615=EDGE_CURVE('',#2817,#2822,#2008,.T.);
#3616=EDGE_CURVE('',#2823,#2824,#1522,.T.);
#3617=EDGE_CURVE('',#2824,#2823,#1523,.T.);
#3618=EDGE_CURVE('',#2824,#2819,#2009,.T.);
#3619=EDGE_CURVE('',#2825,#2826,#1524,.T.);
#3620=EDGE_CURVE('',#2826,#2825,#1525,.T.);
#3621=EDGE_CURVE('',#2826,#2827,#2010,.T.);
#3622=EDGE_CURVE('',#2827,#2828,#1526,.T.);
#3623=EDGE_CURVE('',#2828,#2827,#1527,.T.);
#3624=EDGE_CURVE('',#2823,#2828,#2011,.T.);
#3625=EDGE_CURVE('',#2829,#2830,#1528,.T.);
#3626=EDGE_CURVE('',#2830,#2829,#1529,.T.);
#3627=EDGE_CURVE('',#2830,#2825,#2012,.T.);
#3628=EDGE_CURVE('',#2831,#2832,#1530,.T.);
#3629=EDGE_CURVE('',#2832,#2831,#1531,.T.);
#3630=EDGE_CURVE('',#2832,#2833,#2013,.T.);
#3631=EDGE_CURVE('',#2833,#2834,#1532,.T.);
#3632=EDGE_CURVE('',#2834,#2833,#1533,.T.);
#3633=EDGE_CURVE('',#2829,#2834,#2014,.T.);
#3634=EDGE_CURVE('',#2835,#2836,#1534,.T.);
#3635=EDGE_CURVE('',#2836,#2835,#1535,.T.);
#3636=EDGE_CURVE('',#2836,#2831,#2015,.T.);
#3637=EDGE_CURVE('',#2837,#2838,#1536,.T.);
#3638=EDGE_CURVE('',#2838,#2837,#1537,.T.);
#3639=EDGE_CURVE('',#2838,#2839,#2016,.T.);
#3640=EDGE_CURVE('',#2839,#2840,#1538,.T.);
#3641=EDGE_CURVE('',#2840,#2839,#1539,.T.);
#3642=EDGE_CURVE('',#2835,#2840,#2017,.T.);
#3643=EDGE_CURVE('',#2841,#2842,#1540,.T.);
#3644=EDGE_CURVE('',#2842,#2841,#1541,.T.);
#3645=EDGE_CURVE('',#2842,#2837,#2018,.T.);
#3646=EDGE_CURVE('',#2843,#2844,#1542,.T.);
#3647=EDGE_CURVE('',#2844,#2843,#1543,.T.);
#3648=EDGE_CURVE('',#2844,#2845,#2019,.T.);
#3649=EDGE_CURVE('',#2845,#2846,#1544,.T.);
#3650=EDGE_CURVE('',#2846,#2845,#1545,.T.);
#3651=EDGE_CURVE('',#2841,#2846,#2020,.T.);
#3652=EDGE_CURVE('',#2847,#2848,#1546,.T.);
#3653=EDGE_CURVE('',#2848,#2847,#1547,.T.);
#3654=EDGE_CURVE('',#2848,#2843,#2021,.T.);
#3655=EDGE_CURVE('',#2849,#2850,#1548,.T.);
#3656=EDGE_CURVE('',#2850,#2849,#1549,.T.);
#3657=EDGE_CURVE('',#2850,#2851,#2022,.T.);
#3658=EDGE_CURVE('',#2851,#2852,#1550,.T.);
#3659=EDGE_CURVE('',#2852,#2851,#1551,.T.);
#3660=EDGE_CURVE('',#2847,#2852,#2023,.T.);
#3661=EDGE_CURVE('',#2853,#2854,#1552,.T.);
#3662=EDGE_CURVE('',#2854,#2853,#1553,.T.);
#3663=EDGE_CURVE('',#2854,#2849,#2024,.T.);
#3664=EDGE_CURVE('',#2855,#2856,#1554,.T.);
#3665=EDGE_CURVE('',#2856,#2855,#1555,.T.);
#3666=EDGE_CURVE('',#2856,#2857,#2025,.T.);
#3667=EDGE_CURVE('',#2857,#2858,#1556,.T.);
#3668=EDGE_CURVE('',#2858,#2857,#1557,.T.);
#3669=EDGE_CURVE('',#2853,#2858,#2026,.T.);
#3670=EDGE_CURVE('',#2859,#2860,#1558,.T.);
#3671=EDGE_CURVE('',#2860,#2859,#1559,.T.);
#3672=EDGE_CURVE('',#2860,#2855,#2027,.T.);
#3673=EDGE_CURVE('',#2861,#2862,#1560,.T.);
#3674=EDGE_CURVE('',#2862,#2861,#1561,.T.);
#3675=EDGE_CURVE('',#2862,#2863,#2028,.T.);
#3676=EDGE_CURVE('',#2863,#2864,#1562,.T.);
#3677=EDGE_CURVE('',#2864,#2863,#1563,.T.);
#3678=EDGE_CURVE('',#2859,#2864,#2029,.T.);
#3679=EDGE_CURVE('',#2865,#2866,#1564,.T.);
#3680=EDGE_CURVE('',#2866,#2865,#1565,.T.);
#3681=EDGE_CURVE('',#2866,#2861,#2030,.T.);
#3682=EDGE_CURVE('',#2867,#2868,#1566,.T.);
#3683=EDGE_CURVE('',#2868,#2867,#1567,.T.);
#3684=EDGE_CURVE('',#2868,#2869,#2031,.T.);
#3685=EDGE_CURVE('',#2869,#2870,#1568,.T.);
#3686=EDGE_CURVE('',#2870,#2869,#1569,.T.);
#3687=EDGE_CURVE('',#2865,#2870,#2032,.T.);
#3688=EDGE_CURVE('',#2871,#2872,#1570,.T.);
#3689=EDGE_CURVE('',#2872,#2871,#1571,.T.);
#3690=EDGE_CURVE('',#2872,#2867,#2033,.T.);
#3691=EDGE_CURVE('',#2873,#2874,#1572,.T.);
#3692=EDGE_CURVE('',#2874,#2873,#1573,.T.);
#3693=EDGE_CURVE('',#2874,#2875,#2034,.T.);
#3694=EDGE_CURVE('',#2875,#2876,#1574,.T.);
#3695=EDGE_CURVE('',#2876,#2875,#1575,.T.);
#3696=EDGE_CURVE('',#2871,#2876,#2035,.T.);
#3697=EDGE_CURVE('',#2877,#2878,#1576,.T.);
#3698=EDGE_CURVE('',#2878,#2877,#1577,.T.);
#3699=EDGE_CURVE('',#2878,#2873,#2036,.T.);
#3700=EDGE_CURVE('',#2879,#2880,#1578,.T.);
#3701=EDGE_CURVE('',#2880,#2879,#1579,.T.);
#3702=EDGE_CURVE('',#2880,#2881,#2037,.T.);
#3703=EDGE_CURVE('',#2881,#2882,#1580,.T.);
#3704=EDGE_CURVE('',#2882,#2881,#1581,.T.);
#3705=EDGE_CURVE('',#2877,#2882,#2038,.T.);
#3706=EDGE_CURVE('',#2883,#2884,#1582,.T.);
#3707=EDGE_CURVE('',#2884,#2883,#1583,.T.);
#3708=EDGE_CURVE('',#2884,#2879,#2039,.T.);
#3709=EDGE_CURVE('',#2885,#2886,#1584,.T.);
#3710=EDGE_CURVE('',#2886,#2885,#1585,.T.);
#3711=EDGE_CURVE('',#2886,#2887,#2040,.T.);
#3712=EDGE_CURVE('',#2887,#2888,#1586,.T.);
#3713=EDGE_CURVE('',#2888,#2887,#1587,.T.);
#3714=EDGE_CURVE('',#2883,#2888,#2041,.T.);
#3715=EDGE_CURVE('',#2889,#2890,#1588,.T.);
#3716=EDGE_CURVE('',#2890,#2889,#1589,.T.);
#3717=EDGE_CURVE('',#2890,#2885,#2042,.T.);
#3718=EDGE_CURVE('',#2891,#2892,#1590,.T.);
#3719=EDGE_CURVE('',#2892,#2891,#1591,.T.);
#3720=EDGE_CURVE('',#2892,#2893,#2043,.T.);
#3721=EDGE_CURVE('',#2893,#2894,#1592,.T.);
#3722=EDGE_CURVE('',#2894,#2893,#1593,.T.);
#3723=EDGE_CURVE('',#2889,#2894,#2044,.T.);
#3724=EDGE_CURVE('',#2895,#2896,#1594,.T.);
#3725=EDGE_CURVE('',#2896,#2895,#1595,.T.);
#3726=EDGE_CURVE('',#2896,#2891,#2045,.T.);
#3727=EDGE_CURVE('',#2897,#2898,#1596,.T.);
#3728=EDGE_CURVE('',#2898,#2897,#1597,.T.);
#3729=EDGE_CURVE('',#2898,#2899,#2046,.T.);
#3730=EDGE_CURVE('',#2899,#2900,#1598,.T.);
#3731=EDGE_CURVE('',#2900,#2899,#1599,.T.);
#3732=EDGE_CURVE('',#2895,#2900,#2047,.T.);
#3733=EDGE_CURVE('',#2901,#2902,#1600,.T.);
#3734=EDGE_CURVE('',#2902,#2901,#1601,.T.);
#3735=EDGE_CURVE('',#2902,#2897,#2048,.T.);
#3736=EDGE_CURVE('',#2903,#2904,#1602,.T.);
#3737=EDGE_CURVE('',#2904,#2903,#1603,.T.);
#3738=EDGE_CURVE('',#2904,#2905,#2049,.T.);
#3739=EDGE_CURVE('',#2905,#2906,#1604,.T.);
#3740=EDGE_CURVE('',#2906,#2905,#1605,.T.);
#3741=EDGE_CURVE('',#2901,#2906,#2050,.T.);
#3742=EDGE_CURVE('',#2907,#2908,#1606,.T.);
#3743=EDGE_CURVE('',#2908,#2907,#1607,.T.);
#3744=EDGE_CURVE('',#2908,#2909,#1608,.T.);
#3745=EDGE_CURVE('',#2909,#2909,#1609,.T.);
#3746=EDGE_CURVE('',#2910,#2911,#1610,.T.);
#3747=EDGE_CURVE('',#2912,#2910,#1611,.T.);
#3748=EDGE_CURVE('',#2913,#2912,#1612,.T.);
#3749=EDGE_CURVE('',#2913,#2914,#2051,.T.);
#3750=EDGE_CURVE('',#2914,#2914,#1613,.T.);
#3751=EDGE_CURVE('',#2915,#2913,#1614,.T.);
#3752=EDGE_CURVE('',#2916,#2915,#1615,.T.);
#3753=EDGE_CURVE('',#2911,#2916,#1616,.T.);
#3754=EDGE_CURVE('',#2907,#2903,#2052,.T.);
#3755=EDGE_CURVE('',#2917,#2915,#2053,.T.);
#3756=EDGE_CURVE('',#2913,#2917,#2054,.T.);
#3757=EDGE_CURVE('',#2915,#2918,#2055,.T.);
#3758=EDGE_CURVE('',#2918,#2916,#2056,.T.);
#3759=EDGE_CURVE('',#2916,#2919,#2057,.T.);
#3760=EDGE_CURVE('',#2919,#2911,#2058,.T.);
#3761=EDGE_CURVE('',#2911,#2920,#2059,.T.);
#3762=EDGE_CURVE('',#2920,#2910,#2060,.T.);
#3763=EDGE_CURVE('',#2910,#2921,#2061,.T.);
#3764=EDGE_CURVE('',#2921,#2912,#2062,.T.);
#3765=EDGE_CURVE('',#2912,#2922,#2063,.T.);
#3766=EDGE_CURVE('',#2922,#2913,#2064,.T.);
#3767=EDGE_CURVE('',#2923,#2924,#1617,.T.);
#3768=EDGE_CURVE('',#2925,#2923,#1618,.T.);
#3769=EDGE_CURVE('',#2926,#2925,#1619,.T.);
#3770=EDGE_CURVE('',#2927,#2926,#1620,.T.);
#3771=EDGE_CURVE('',#2927,#2928,#1621,.T.);
#3772=EDGE_CURVE('',#2924,#2928,#1622,.T.);
#3773=EDGE_CURVE('',#2928,#2929,#237,.T.);
#3774=EDGE_CURVE('',#2929,#2924,#238,.T.);
#3775=EDGE_CURVE('',#2927,#2930,#239,.T.);
#3776=EDGE_CURVE('',#2930,#2928,#240,.T.);
#3777=EDGE_CURVE('',#2931,#2927,#241,.T.);
#3778=EDGE_CURVE('',#2926,#2931,#242,.T.);
#3779=EDGE_CURVE('',#2932,#2926,#243,.T.);
#3780=EDGE_CURVE('',#2925,#2932,#244,.T.);
#3781=EDGE_CURVE('',#2924,#2933,#245,.T.);
#3782=EDGE_CURVE('',#2933,#2923,#246,.T.);
#3783=EDGE_CURVE('',#2934,#2925,#247,.T.);
#3784=EDGE_CURVE('',#2923,#2934,#248,.T.);
#3785=EDGE_CURVE('',#2922,#2934,#2065,.T.);
#3786=EDGE_CURVE('',#2917,#2933,#2066,.T.);
#3787=EDGE_CURVE('',#2921,#2932,#2067,.T.);
#3788=EDGE_CURVE('',#2920,#2931,#2068,.T.);
#3789=EDGE_CURVE('',#2919,#2930,#2069,.T.);
#3790=EDGE_CURVE('',#2918,#2929,#2070,.T.);
#5108=ORIENTED_EDGE('',*,*,#3606,.T.);
#5109=ORIENTED_EDGE('',*,*,#3607,.T.);
#5110=ORIENTED_EDGE('',*,*,#3608,.T.);
#5111=ORIENTED_EDGE('',*,*,#3609,.T.);
#5112=ORIENTED_EDGE('',*,*,#3608,.F.);
#5113=ORIENTED_EDGE('',*,*,#3610,.F.);
#5114=ORIENTED_EDGE('',*,*,#3611,.F.);
#5115=ORIENTED_EDGE('',*,*,#3612,.T.);
#5116=ORIENTED_EDGE('',*,*,#3613,.T.);
#5117=ORIENTED_EDGE('',*,*,#3614,.T.);
#5118=ORIENTED_EDGE('',*,*,#3612,.F.);
#5119=ORIENTED_EDGE('',*,*,#3606,.F.);
#5120=ORIENTED_EDGE('',*,*,#3607,.F.);
#5121=ORIENTED_EDGE('',*,*,#3615,.T.);
#5122=ORIENTED_EDGE('',*,*,#3613,.F.);
#5123=ORIENTED_EDGE('',*,*,#3614,.F.);
#5124=ORIENTED_EDGE('',*,*,#3615,.F.);
#5125=ORIENTED_EDGE('',*,*,#3616,.F.);
#5126=ORIENTED_EDGE('',*,*,#3617,.F.);
#5127=ORIENTED_EDGE('',*,*,#3618,.T.);
#5128=ORIENTED_EDGE('',*,*,#3610,.T.);
#5129=ORIENTED_EDGE('',*,*,#3611,.T.);
#5130=ORIENTED_EDGE('',*,*,#3618,.F.);
#5131=ORIENTED_EDGE('',*,*,#3619,.F.);
#5132=ORIENTED_EDGE('',*,*,#3620,.F.);
#5133=ORIENTED_EDGE('',*,*,#3621,.T.);
#5134=ORIENTED_EDGE('',*,*,#3622,.T.);
#5135=ORIENTED_EDGE('',*,*,#3623,.T.);
#5136=ORIENTED_EDGE('',*,*,#3621,.F.);
#5137=ORIENTED_EDGE('',*,*,#3616,.T.);
#5138=ORIENTED_EDGE('',*,*,#3617,.T.);
#5139=ORIENTED_EDGE('',*,*,#3624,.T.);
#5140=ORIENTED_EDGE('',*,*,#3622,.F.);
#5141=ORIENTED_EDGE('',*,*,#3623,.F.);
#5142=ORIENTED_EDGE('',*,*,#3624,.F.);
#5143=ORIENTED_EDGE('',*,*,#3625,.F.);
#5144=ORIENTED_EDGE('',*,*,#3626,.F.);
#5145=ORIENTED_EDGE('',*,*,#3627,.T.);
#5146=ORIENTED_EDGE('',*,*,#3619,.T.);
#5147=ORIENTED_EDGE('',*,*,#3620,.T.);
#5148=ORIENTED_EDGE('',*,*,#3627,.F.);
#5149=ORIENTED_EDGE('',*,*,#3628,.F.);
#5150=ORIENTED_EDGE('',*,*,#3629,.F.);
#5151=ORIENTED_EDGE('',*,*,#3630,.T.);
#5152=ORIENTED_EDGE('',*,*,#3631,.T.);
#5153=ORIENTED_EDGE('',*,*,#3632,.T.);
#5154=ORIENTED_EDGE('',*,*,#3630,.F.);
#5155=ORIENTED_EDGE('',*,*,#3625,.T.);
#5156=ORIENTED_EDGE('',*,*,#3626,.T.);
#5157=ORIENTED_EDGE('',*,*,#3633,.T.);
#5158=ORIENTED_EDGE('',*,*,#3631,.F.);
#5159=ORIENTED_EDGE('',*,*,#3632,.F.);
#5160=ORIENTED_EDGE('',*,*,#3633,.F.);
#5161=ORIENTED_EDGE('',*,*,#3634,.F.);
#5162=ORIENTED_EDGE('',*,*,#3635,.F.);
#5163=ORIENTED_EDGE('',*,*,#3636,.T.);
#5164=ORIENTED_EDGE('',*,*,#3628,.T.);
#5165=ORIENTED_EDGE('',*,*,#3629,.T.);
#5166=ORIENTED_EDGE('',*,*,#3636,.F.);
#5167=ORIENTED_EDGE('',*,*,#3637,.F.);
#5168=ORIENTED_EDGE('',*,*,#3638,.F.);
#5169=ORIENTED_EDGE('',*,*,#3639,.T.);
#5170=ORIENTED_EDGE('',*,*,#3640,.T.);
#5171=ORIENTED_EDGE('',*,*,#3641,.T.);
#5172=ORIENTED_EDGE('',*,*,#3639,.F.);
#5173=ORIENTED_EDGE('',*,*,#3634,.T.);
#5174=ORIENTED_EDGE('',*,*,#3635,.T.);
#5175=ORIENTED_EDGE('',*,*,#3642,.T.);
#5176=ORIENTED_EDGE('',*,*,#3640,.F.);
#5177=ORIENTED_EDGE('',*,*,#3641,.F.);
#5178=ORIENTED_EDGE('',*,*,#3642,.F.);
#5179=ORIENTED_EDGE('',*,*,#3643,.F.);
#5180=ORIENTED_EDGE('',*,*,#3644,.F.);
#5181=ORIENTED_EDGE('',*,*,#3645,.T.);
#5182=ORIENTED_EDGE('',*,*,#3637,.T.);
#5183=ORIENTED_EDGE('',*,*,#3638,.T.);
#5184=ORIENTED_EDGE('',*,*,#3645,.F.);
#5185=ORIENTED_EDGE('',*,*,#3646,.F.);
#5186=ORIENTED_EDGE('',*,*,#3647,.F.);
#5187=ORIENTED_EDGE('',*,*,#3648,.T.);
#5188=ORIENTED_EDGE('',*,*,#3649,.T.);
#5189=ORIENTED_EDGE('',*,*,#3650,.T.);
#5190=ORIENTED_EDGE('',*,*,#3648,.F.);
#5191=ORIENTED_EDGE('',*,*,#3643,.T.);
#5192=ORIENTED_EDGE('',*,*,#3644,.T.);
#5193=ORIENTED_EDGE('',*,*,#3651,.T.);
#5194=ORIENTED_EDGE('',*,*,#3649,.F.);
#5195=ORIENTED_EDGE('',*,*,#3650,.F.);
#5196=ORIENTED_EDGE('',*,*,#3651,.F.);
#5197=ORIENTED_EDGE('',*,*,#3652,.F.);
#5198=ORIENTED_EDGE('',*,*,#3653,.F.);
#5199=ORIENTED_EDGE('',*,*,#3654,.T.);
#5200=ORIENTED_EDGE('',*,*,#3646,.T.);
#5201=ORIENTED_EDGE('',*,*,#3647,.T.);
#5202=ORIENTED_EDGE('',*,*,#3654,.F.);
#5203=ORIENTED_EDGE('',*,*,#3655,.F.);
#5204=ORIENTED_EDGE('',*,*,#3656,.F.);
#5205=ORIENTED_EDGE('',*,*,#3657,.T.);
#5206=ORIENTED_EDGE('',*,*,#3658,.T.);
#5207=ORIENTED_EDGE('',*,*,#3659,.T.);
#5208=ORIENTED_EDGE('',*,*,#3657,.F.);
#5209=ORIENTED_EDGE('',*,*,#3652,.T.);
#5210=ORIENTED_EDGE('',*,*,#3653,.T.);
#5211=ORIENTED_EDGE('',*,*,#3660,.T.);
#5212=ORIENTED_EDGE('',*,*,#3658,.F.);
#5213=ORIENTED_EDGE('',*,*,#3659,.F.);
#5214=ORIENTED_EDGE('',*,*,#3660,.F.);
#5215=ORIENTED_EDGE('',*,*,#3661,.F.);
#5216=ORIENTED_EDGE('',*,*,#3662,.F.);
#5217=ORIENTED_EDGE('',*,*,#3663,.T.);
#5218=ORIENTED_EDGE('',*,*,#3655,.T.);
#5219=ORIENTED_EDGE('',*,*,#3656,.T.);
#5220=ORIENTED_EDGE('',*,*,#3663,.F.);
#5221=ORIENTED_EDGE('',*,*,#3664,.F.);
#5222=ORIENTED_EDGE('',*,*,#3665,.F.);
#5223=ORIENTED_EDGE('',*,*,#3666,.T.);
#5224=ORIENTED_EDGE('',*,*,#3667,.T.);
#5225=ORIENTED_EDGE('',*,*,#3668,.T.);
#5226=ORIENTED_EDGE('',*,*,#3666,.F.);
#5227=ORIENTED_EDGE('',*,*,#3661,.T.);
#5228=ORIENTED_EDGE('',*,*,#3662,.T.);
#5229=ORIENTED_EDGE('',*,*,#3669,.T.);
#5230=ORIENTED_EDGE('',*,*,#3667,.F.);
#5231=ORIENTED_EDGE('',*,*,#3668,.F.);
#5232=ORIENTED_EDGE('',*,*,#3669,.F.);
#5233=ORIENTED_EDGE('',*,*,#3670,.F.);
#5234=ORIENTED_EDGE('',*,*,#3671,.F.);
#5235=ORIENTED_EDGE('',*,*,#3672,.T.);
#5236=ORIENTED_EDGE('',*,*,#3664,.T.);
#5237=ORIENTED_EDGE('',*,*,#3665,.T.);
#5238=ORIENTED_EDGE('',*,*,#3672,.F.);
#5239=ORIENTED_EDGE('',*,*,#3673,.F.);
#5240=ORIENTED_EDGE('',*,*,#3674,.F.);
#5241=ORIENTED_EDGE('',*,*,#3675,.T.);
#5242=ORIENTED_EDGE('',*,*,#3676,.T.);
#5243=ORIENTED_EDGE('',*,*,#3677,.T.);
#5244=ORIENTED_EDGE('',*,*,#3675,.F.);
#5245=ORIENTED_EDGE('',*,*,#3670,.T.);
#5246=ORIENTED_EDGE('',*,*,#3671,.T.);
#5247=ORIENTED_EDGE('',*,*,#3678,.T.);
#5248=ORIENTED_EDGE('',*,*,#3676,.F.);
#5249=ORIENTED_EDGE('',*,*,#3677,.F.);
#5250=ORIENTED_EDGE('',*,*,#3678,.F.);
#5251=ORIENTED_EDGE('',*,*,#3679,.F.);
#5252=ORIENTED_EDGE('',*,*,#3680,.F.);
#5253=ORIENTED_EDGE('',*,*,#3681,.T.);
#5254=ORIENTED_EDGE('',*,*,#3673,.T.);
#5255=ORIENTED_EDGE('',*,*,#3674,.T.);
#5256=ORIENTED_EDGE('',*,*,#3681,.F.);
#5257=ORIENTED_EDGE('',*,*,#3682,.F.);
#5258=ORIENTED_EDGE('',*,*,#3683,.F.);
#5259=ORIENTED_EDGE('',*,*,#3684,.T.);
#5260=ORIENTED_EDGE('',*,*,#3685,.T.);
#5261=ORIENTED_EDGE('',*,*,#3686,.T.);
#5262=ORIENTED_EDGE('',*,*,#3684,.F.);
#5263=ORIENTED_EDGE('',*,*,#3679,.T.);
#5264=ORIENTED_EDGE('',*,*,#3680,.T.);
#5265=ORIENTED_EDGE('',*,*,#3687,.T.);
#5266=ORIENTED_EDGE('',*,*,#3685,.F.);
#5267=ORIENTED_EDGE('',*,*,#3686,.F.);
#5268=ORIENTED_EDGE('',*,*,#3687,.F.);
#5269=ORIENTED_EDGE('',*,*,#3688,.F.);
#5270=ORIENTED_EDGE('',*,*,#3689,.F.);
#5271=ORIENTED_EDGE('',*,*,#3690,.T.);
#5272=ORIENTED_EDGE('',*,*,#3682,.T.);
#5273=ORIENTED_EDGE('',*,*,#3683,.T.);
#5274=ORIENTED_EDGE('',*,*,#3690,.F.);
#5275=ORIENTED_EDGE('',*,*,#3691,.F.);
#5276=ORIENTED_EDGE('',*,*,#3692,.F.);
#5277=ORIENTED_EDGE('',*,*,#3693,.T.);
#5278=ORIENTED_EDGE('',*,*,#3694,.T.);
#5279=ORIENTED_EDGE('',*,*,#3695,.T.);
#5280=ORIENTED_EDGE('',*,*,#3693,.F.);
#5281=ORIENTED_EDGE('',*,*,#3688,.T.);
#5282=ORIENTED_EDGE('',*,*,#3689,.T.);
#5283=ORIENTED_EDGE('',*,*,#3696,.T.);
#5284=ORIENTED_EDGE('',*,*,#3694,.F.);
#5285=ORIENTED_EDGE('',*,*,#3695,.F.);
#5286=ORIENTED_EDGE('',*,*,#3696,.F.);
#5287=ORIENTED_EDGE('',*,*,#3697,.F.);
#5288=ORIENTED_EDGE('',*,*,#3698,.F.);
#5289=ORIENTED_EDGE('',*,*,#3699,.T.);
#5290=ORIENTED_EDGE('',*,*,#3691,.T.);
#5291=ORIENTED_EDGE('',*,*,#3692,.T.);
#5292=ORIENTED_EDGE('',*,*,#3699,.F.);
#5293=ORIENTED_EDGE('',*,*,#3700,.F.);
#5294=ORIENTED_EDGE('',*,*,#3701,.F.);
#5295=ORIENTED_EDGE('',*,*,#3702,.T.);
#5296=ORIENTED_EDGE('',*,*,#3703,.T.);
#5297=ORIENTED_EDGE('',*,*,#3704,.T.);
#5298=ORIENTED_EDGE('',*,*,#3702,.F.);
#5299=ORIENTED_EDGE('',*,*,#3697,.T.);
#5300=ORIENTED_EDGE('',*,*,#3698,.T.);
#5301=ORIENTED_EDGE('',*,*,#3705,.T.);
#5302=ORIENTED_EDGE('',*,*,#3703,.F.);
#5303=ORIENTED_EDGE('',*,*,#3704,.F.);
#5304=ORIENTED_EDGE('',*,*,#3705,.F.);
#5305=ORIENTED_EDGE('',*,*,#3706,.F.);
#5306=ORIENTED_EDGE('',*,*,#3707,.F.);
#5307=ORIENTED_EDGE('',*,*,#3708,.T.);
#5308=ORIENTED_EDGE('',*,*,#3700,.T.);
#5309=ORIENTED_EDGE('',*,*,#3701,.T.);
#5310=ORIENTED_EDGE('',*,*,#3708,.F.);
#5311=ORIENTED_EDGE('',*,*,#3709,.F.);
#5312=ORIENTED_EDGE('',*,*,#3710,.F.);
#5313=ORIENTED_EDGE('',*,*,#3711,.T.);
#5314=ORIENTED_EDGE('',*,*,#3712,.T.);
#5315=ORIENTED_EDGE('',*,*,#3713,.T.);
#5316=ORIENTED_EDGE('',*,*,#3711,.F.);
#5317=ORIENTED_EDGE('',*,*,#3706,.T.);
#5318=ORIENTED_EDGE('',*,*,#3707,.T.);
#5319=ORIENTED_EDGE('',*,*,#3714,.T.);
#5320=ORIENTED_EDGE('',*,*,#3712,.F.);
#5321=ORIENTED_EDGE('',*,*,#3713,.F.);
#5322=ORIENTED_EDGE('',*,*,#3714,.F.);
#5323=ORIENTED_EDGE('',*,*,#3715,.F.);
#5324=ORIENTED_EDGE('',*,*,#3716,.F.);
#5325=ORIENTED_EDGE('',*,*,#3717,.T.);
#5326=ORIENTED_EDGE('',*,*,#3709,.T.);
#5327=ORIENTED_EDGE('',*,*,#3710,.T.);
#5328=ORIENTED_EDGE('',*,*,#3717,.F.);
#5329=ORIENTED_EDGE('',*,*,#3718,.F.);
#5330=ORIENTED_EDGE('',*,*,#3719,.F.);
#5331=ORIENTED_EDGE('',*,*,#3720,.T.);
#5332=ORIENTED_EDGE('',*,*,#3721,.T.);
#5333=ORIENTED_EDGE('',*,*,#3722,.T.);
#5334=ORIENTED_EDGE('',*,*,#3720,.F.);
#5335=ORIENTED_EDGE('',*,*,#3715,.T.);
#5336=ORIENTED_EDGE('',*,*,#3716,.T.);
#5337=ORIENTED_EDGE('',*,*,#3723,.T.);
#5338=ORIENTED_EDGE('',*,*,#3721,.F.);
#5339=ORIENTED_EDGE('',*,*,#3722,.F.);
#5340=ORIENTED_EDGE('',*,*,#3723,.F.);
#5341=ORIENTED_EDGE('',*,*,#3724,.F.);
#5342=ORIENTED_EDGE('',*,*,#3725,.F.);
#5343=ORIENTED_EDGE('',*,*,#3726,.T.);
#5344=ORIENTED_EDGE('',*,*,#3718,.T.);
#5345=ORIENTED_EDGE('',*,*,#3719,.T.);
#5346=ORIENTED_EDGE('',*,*,#3726,.F.);
#5347=ORIENTED_EDGE('',*,*,#3727,.F.);
#5348=ORIENTED_EDGE('',*,*,#3728,.F.);
#5349=ORIENTED_EDGE('',*,*,#3729,.T.);
#5350=ORIENTED_EDGE('',*,*,#3730,.T.);
#5351=ORIENTED_EDGE('',*,*,#3731,.T.);
#5352=ORIENTED_EDGE('',*,*,#3729,.F.);
#5353=ORIENTED_EDGE('',*,*,#3724,.T.);
#5354=ORIENTED_EDGE('',*,*,#3725,.T.);
#5355=ORIENTED_EDGE('',*,*,#3732,.T.);
#5356=ORIENTED_EDGE('',*,*,#3730,.F.);
#5357=ORIENTED_EDGE('',*,*,#3731,.F.);
#5358=ORIENTED_EDGE('',*,*,#3732,.F.);
#5359=ORIENTED_EDGE('',*,*,#3733,.F.);
#5360=ORIENTED_EDGE('',*,*,#3734,.F.);
#5361=ORIENTED_EDGE('',*,*,#3735,.T.);
#5362=ORIENTED_EDGE('',*,*,#3727,.T.);
#5363=ORIENTED_EDGE('',*,*,#3728,.T.);
#5364=ORIENTED_EDGE('',*,*,#3735,.F.);
#5365=ORIENTED_EDGE('',*,*,#3736,.F.);
#5366=ORIENTED_EDGE('',*,*,#3737,.F.);
#5367=ORIENTED_EDGE('',*,*,#3738,.T.);
#5368=ORIENTED_EDGE('',*,*,#3739,.T.);
#5369=ORIENTED_EDGE('',*,*,#3740,.T.);
#5370=ORIENTED_EDGE('',*,*,#3738,.F.);
#5371=ORIENTED_EDGE('',*,*,#3733,.T.);
#5372=ORIENTED_EDGE('',*,*,#3734,.T.);
#5373=ORIENTED_EDGE('',*,*,#3741,.T.);
#5374=ORIENTED_EDGE('',*,*,#3739,.F.);
#5375=ORIENTED_EDGE('',*,*,#3740,.F.);
#5376=ORIENTED_EDGE('',*,*,#3741,.F.);
#5377=ORIENTED_EDGE('',*,*,#3742,.F.);
#5378=ORIENTED_EDGE('',*,*,#3743,.F.);
#5379=ORIENTED_EDGE('',*,*,#3744,.T.);
#5380=ORIENTED_EDGE('',*,*,#3745,.F.);
#5381=ORIENTED_EDGE('',*,*,#3744,.F.);
#5382=ORIENTED_EDGE('',*,*,#3746,.F.);
#5383=ORIENTED_EDGE('',*,*,#3747,.F.);
#5384=ORIENTED_EDGE('',*,*,#3748,.F.);
#5385=ORIENTED_EDGE('',*,*,#3749,.T.);
#5386=ORIENTED_EDGE('',*,*,#3750,.F.);
#5387=ORIENTED_EDGE('',*,*,#3749,.F.);
#5388=ORIENTED_EDGE('',*,*,#3751,.F.);
#5389=ORIENTED_EDGE('',*,*,#3752,.F.);
#5390=ORIENTED_EDGE('',*,*,#3753,.F.);
#5391=ORIENTED_EDGE('',*,*,#3742,.T.);
#5392=ORIENTED_EDGE('',*,*,#3743,.T.);
#5393=ORIENTED_EDGE('',*,*,#3754,.T.);
#5394=ORIENTED_EDGE('',*,*,#3736,.T.);
#5395=ORIENTED_EDGE('',*,*,#3737,.T.);
#5396=ORIENTED_EDGE('',*,*,#3754,.F.);
#5397=ORIENTED_EDGE('',*,*,#3750,.T.);
#5398=ORIENTED_EDGE('',*,*,#3745,.T.);
#5399=ORIENTED_EDGE('',*,*,#3755,.T.);
#5400=ORIENTED_EDGE('',*,*,#3751,.T.);
#5401=ORIENTED_EDGE('',*,*,#3756,.T.);
#5402=ORIENTED_EDGE('',*,*,#3757,.T.);
#5403=ORIENTED_EDGE('',*,*,#3758,.T.);
#5404=ORIENTED_EDGE('',*,*,#3752,.T.);
#5405=ORIENTED_EDGE('',*,*,#3759,.T.);
#5406=ORIENTED_EDGE('',*,*,#3760,.T.);
#5407=ORIENTED_EDGE('',*,*,#3753,.T.);
#5408=ORIENTED_EDGE('',*,*,#3761,.T.);
#5409=ORIENTED_EDGE('',*,*,#3762,.T.);
#5410=ORIENTED_EDGE('',*,*,#3746,.T.);
#5411=ORIENTED_EDGE('',*,*,#3763,.T.);
#5412=ORIENTED_EDGE('',*,*,#3764,.T.);
#5413=ORIENTED_EDGE('',*,*,#3747,.T.);
#5414=ORIENTED_EDGE('',*,*,#3765,.T.);
#5415=ORIENTED_EDGE('',*,*,#3766,.T.);
#5416=ORIENTED_EDGE('',*,*,#3748,.T.);
#5417=ORIENTED_EDGE('',*,*,#3767,.F.);
#5418=ORIENTED_EDGE('',*,*,#3768,.F.);
#5419=ORIENTED_EDGE('',*,*,#3769,.F.);
#5420=ORIENTED_EDGE('',*,*,#3770,.F.);
#5421=ORIENTED_EDGE('',*,*,#3771,.T.);
#5422=ORIENTED_EDGE('',*,*,#3772,.F.);
#5423=ORIENTED_EDGE('',*,*,#3773,.T.);
#5424=ORIENTED_EDGE('',*,*,#3774,.T.);
#5425=ORIENTED_EDGE('',*,*,#3772,.T.);
#5426=ORIENTED_EDGE('',*,*,#3775,.T.);
#5427=ORIENTED_EDGE('',*,*,#3776,.T.);
#5428=ORIENTED_EDGE('',*,*,#3771,.F.);
#5429=ORIENTED_EDGE('',*,*,#3777,.T.);
#5430=ORIENTED_EDGE('',*,*,#3770,.T.);
#5431=ORIENTED_EDGE('',*,*,#3778,.T.);
#5432=ORIENTED_EDGE('',*,*,#3779,.T.);
#5433=ORIENTED_EDGE('',*,*,#3769,.T.);
#5434=ORIENTED_EDGE('',*,*,#3780,.T.);
#5435=ORIENTED_EDGE('',*,*,#3781,.T.);
#5436=ORIENTED_EDGE('',*,*,#3782,.T.);
#5437=ORIENTED_EDGE('',*,*,#3767,.T.);
#5438=ORIENTED_EDGE('',*,*,#3783,.T.);
#5439=ORIENTED_EDGE('',*,*,#3768,.T.);
#5440=ORIENTED_EDGE('',*,*,#3784,.T.);
#5441=ORIENTED_EDGE('',*,*,#3766,.F.);
#5442=ORIENTED_EDGE('',*,*,#3785,.T.);
#5443=ORIENTED_EDGE('',*,*,#3784,.F.);
#5444=ORIENTED_EDGE('',*,*,#3782,.F.);
#5445=ORIENTED_EDGE('',*,*,#3786,.F.);
#5446=ORIENTED_EDGE('',*,*,#3756,.F.);
#5447=ORIENTED_EDGE('',*,*,#3764,.F.);
#5448=ORIENTED_EDGE('',*,*,#3787,.T.);
#5449=ORIENTED_EDGE('',*,*,#3780,.F.);
#5450=ORIENTED_EDGE('',*,*,#3783,.F.);
#5451=ORIENTED_EDGE('',*,*,#3785,.F.);
#5452=ORIENTED_EDGE('',*,*,#3765,.F.);
#5453=ORIENTED_EDGE('',*,*,#3762,.F.);
#5454=ORIENTED_EDGE('',*,*,#3788,.T.);
#5455=ORIENTED_EDGE('',*,*,#3778,.F.);
#5456=ORIENTED_EDGE('',*,*,#3779,.F.);
#5457=ORIENTED_EDGE('',*,*,#3787,.F.);
#5458=ORIENTED_EDGE('',*,*,#3763,.F.);
#5459=ORIENTED_EDGE('',*,*,#3760,.F.);
#5460=ORIENTED_EDGE('',*,*,#3789,.T.);
#5461=ORIENTED_EDGE('',*,*,#3775,.F.);
#5462=ORIENTED_EDGE('',*,*,#3777,.F.);
#5463=ORIENTED_EDGE('',*,*,#3788,.F.);
#5464=ORIENTED_EDGE('',*,*,#3761,.F.);
#5465=ORIENTED_EDGE('',*,*,#3758,.F.);
#5466=ORIENTED_EDGE('',*,*,#3790,.T.);
#5467=ORIENTED_EDGE('',*,*,#3773,.F.);
#5468=ORIENTED_EDGE('',*,*,#3776,.F.);
#5469=ORIENTED_EDGE('',*,*,#3789,.F.);
#5470=ORIENTED_EDGE('',*,*,#3759,.F.);
#5471=ORIENTED_EDGE('',*,*,#3755,.F.);
#5472=ORIENTED_EDGE('',*,*,#3786,.T.);
#5473=ORIENTED_EDGE('',*,*,#3781,.F.);
#5474=ORIENTED_EDGE('',*,*,#3774,.F.);
#5475=ORIENTED_EDGE('',*,*,#3790,.F.);
#5476=ORIENTED_EDGE('',*,*,#3757,.F.);
#5477=ORIENTED_EDGE('',*,*,#3609,.F.);
#5873=CYLINDRICAL_SURFACE('',#6847,3.175);
#5874=CYLINDRICAL_SURFACE('',#6856,3.175);
#5875=CYLINDRICAL_SURFACE('',#6865,3.175);
#5876=CYLINDRICAL_SURFACE('',#6874,3.175);
#5877=CYLINDRICAL_SURFACE('',#6883,3.175);
#5878=CYLINDRICAL_SURFACE('',#6892,3.175);
#5879=CYLINDRICAL_SURFACE('',#6901,3.175);
#5880=CYLINDRICAL_SURFACE('',#6910,3.175);
#5881=CYLINDRICAL_SURFACE('',#6919,3.175);
#5882=CYLINDRICAL_SURFACE('',#6928,3.175);
#5883=CYLINDRICAL_SURFACE('',#6937,3.175);
#5884=CYLINDRICAL_SURFACE('',#6946,3.175);
#5885=CYLINDRICAL_SURFACE('',#6955,3.175);
#5886=CYLINDRICAL_SURFACE('',#6964,3.175);
#5887=CYLINDRICAL_SURFACE('',#6978,5.5626);
#5888=CYLINDRICAL_SURFACE('',#6986,3.175);
#6161=ADVANCED_FACE('',(#746),#407,.T.);
#6162=ADVANCED_FACE('',(#747),#408,.T.);
#6163=ADVANCED_FACE('',(#748),#409,.T.);
#6164=ADVANCED_FACE('',(#749),#5873,.T.);
#6165=ADVANCED_FACE('',(#750),#410,.T.);
#6166=ADVANCED_FACE('',(#751),#411,.T.);
#6167=ADVANCED_FACE('',(#752),#5874,.T.);
#6168=ADVANCED_FACE('',(#753),#412,.T.);
#6169=ADVANCED_FACE('',(#754),#413,.T.);
#6170=ADVANCED_FACE('',(#755),#5875,.T.);
#6171=ADVANCED_FACE('',(#756),#414,.T.);
#6172=ADVANCED_FACE('',(#757),#415,.T.);
#6173=ADVANCED_FACE('',(#758),#5876,.T.);
#6174=ADVANCED_FACE('',(#759),#416,.T.);
#6175=ADVANCED_FACE('',(#760),#417,.T.);
#6176=ADVANCED_FACE('',(#761),#5877,.T.);
#6177=ADVANCED_FACE('',(#762),#418,.T.);
#6178=ADVANCED_FACE('',(#763),#419,.T.);
#6179=ADVANCED_FACE('',(#764),#5878,.T.);
#6180=ADVANCED_FACE('',(#765),#420,.T.);
#6181=ADVANCED_FACE('',(#766),#421,.T.);
#6182=ADVANCED_FACE('',(#767),#5879,.T.);
#6183=ADVANCED_FACE('',(#768),#422,.T.);
#6184=ADVANCED_FACE('',(#769),#423,.T.);
#6185=ADVANCED_FACE('',(#770),#5880,.T.);
#6186=ADVANCED_FACE('',(#771),#424,.T.);
#6187=ADVANCED_FACE('',(#772),#425,.T.);
#6188=ADVANCED_FACE('',(#773),#5881,.T.);
#6189=ADVANCED_FACE('',(#774),#426,.T.);
#6190=ADVANCED_FACE('',(#775),#427,.T.);
#6191=ADVANCED_FACE('',(#776),#5882,.T.);
#6192=ADVANCED_FACE('',(#777),#428,.T.);
#6193=ADVANCED_FACE('',(#778),#429,.T.);
#6194=ADVANCED_FACE('',(#779),#5883,.T.);
#6195=ADVANCED_FACE('',(#780),#430,.T.);
#6196=ADVANCED_FACE('',(#781),#431,.T.);
#6197=ADVANCED_FACE('',(#782),#5884,.T.);
#6198=ADVANCED_FACE('',(#783),#432,.T.);
#6199=ADVANCED_FACE('',(#784),#433,.T.);
#6200=ADVANCED_FACE('',(#785),#5885,.T.);
#6201=ADVANCED_FACE('',(#786),#434,.T.);
#6202=ADVANCED_FACE('',(#787),#435,.T.);
#6203=ADVANCED_FACE('',(#788),#5886,.T.);
#6204=ADVANCED_FACE('',(#789),#436,.T.);
#6205=ADVANCED_FACE('',(#790),#437,.T.);
#6206=ADVANCED_FACE('',(#791),#489,.F.);
#6207=ADVANCED_FACE('',(#792),#5887,.T.);
#6208=ADVANCED_FACE('',(#793),#5888,.T.);
#6209=ADVANCED_FACE('',(#794,#354),#298,.T.);
#6210=ADVANCED_FACE('',(#795),#299,.T.);
#6211=ADVANCED_FACE('',(#796),#300,.T.);
#6212=ADVANCED_FACE('',(#797),#301,.T.);
#6213=ADVANCED_FACE('',(#798),#302,.T.);
#6214=ADVANCED_FACE('',(#799),#303,.T.);
#6215=ADVANCED_FACE('',(#800),#304,.T.);
#6216=ADVANCED_FACE('',(#801),#305,.F.);
#6217=ADVANCED_FACE('',(#802),#438,.T.);
#6218=ADVANCED_FACE('',(#803),#439,.T.);
#6219=ADVANCED_FACE('',(#804),#440,.T.);
#6220=ADVANCED_FACE('',(#805),#441,.T.);
#6221=ADVANCED_FACE('',(#806),#442,.T.);
#6222=ADVANCED_FACE('',(#807),#443,.T.);
#6223=ADVANCED_FACE('',(#808),#306,.F.);
#6224=ADVANCED_FACE('',(#809),#307,.F.);
#6225=ADVANCED_FACE('',(#810),#308,.F.);
#6226=ADVANCED_FACE('',(#811),#309,.F.);
#6227=ADVANCED_FACE('',(#812),#310,.F.);
#6228=ADVANCED_FACE('',(#813),#311,.F.);
#6229=ADVANCED_FACE('',(#814),#312,.F.);
#6303=CLOSED_SHELL('',(#6161,#6162,#6163,#6164,#6165,#6166,#6167,#6168,
#6169,#6170,#6171,#6172,#6173,#6174,#6175,#6176,#6177,#6178,#6179,#6180,
#6181,#6182,#6183,#6184,#6185,#6186,#6187,#6188,#6189,#6190,#6191,#6192,
#6193,#6194,#6195,#6196,#6197,#6198,#6199,#6200,#6201,#6202,#6203,#6204,
#6205,#6206,#6207,#6208,#6209,#6210,#6211,#6212,#6213,#6214,#6215,#6216,
#6217,#6218,#6219,#6220,#6221,#6222,#6223,#6224,#6225,#6226,#6227,#6228,
#6229));
#6836=AXIS2_PLACEMENT_3D('',#40030,#8246,#8247);
#6837=AXIS2_PLACEMENT_3D('',#40031,#8248,#8249);
#6838=AXIS2_PLACEMENT_3D('',#40034,#8250,#8251);
#6839=AXIS2_PLACEMENT_3D('',#40035,#8252,#8253);
#6840=AXIS2_PLACEMENT_3D('',#40038,#8255,#8256);
#6841=AXIS2_PLACEMENT_3D('',#40039,#8257,#8258);
#6842=AXIS2_PLACEMENT_3D('',#40042,#8259,#8260);
#6843=AXIS2_PLACEMENT_3D('',#40043,#8261,#8262);
#6844=AXIS2_PLACEMENT_3D('',#40047,#8264,#8265);
#6845=AXIS2_PLACEMENT_3D('',#40048,#8266,#8267);
#6846=AXIS2_PLACEMENT_3D('',#40049,#8268,#8269);
#6847=AXIS2_PLACEMENT_3D('',#40051,#8271,#8272);
#6848=AXIS2_PLACEMENT_3D('',#40054,#8273,#8274);
#6849=AXIS2_PLACEMENT_3D('',#40055,#8275,#8276);
#6850=AXIS2_PLACEMENT_3D('',#40057,#8278,#8279);
#6851=AXIS2_PLACEMENT_3D('',#40060,#8280,#8281);
#6852=AXIS2_PLACEMENT_3D('',#40061,#8282,#8283);
#6853=AXIS2_PLACEMENT_3D('',#40065,#8285,#8286);
#6854=AXIS2_PLACEMENT_3D('',#40066,#8287,#8288);
#6855=AXIS2_PLACEMENT_3D('',#40067,#8289,#8290);
#6856=AXIS2_PLACEMENT_3D('',#40069,#8292,#8293);
#6857=AXIS2_PLACEMENT_3D('',#40072,#8294,#8295);
#6858=AXIS2_PLACEMENT_3D('',#40073,#8296,#8297);
#6859=AXIS2_PLACEMENT_3D('',#40075,#8299,#8300);
#6860=AXIS2_PLACEMENT_3D('',#40078,#8301,#8302);
#6861=AXIS2_PLACEMENT_3D('',#40079,#8303,#8304);
#6862=AXIS2_PLACEMENT_3D('',#40083,#8306,#8307);
#6863=AXIS2_PLACEMENT_3D('',#40084,#8308,#8309);
#6864=AXIS2_PLACEMENT_3D('',#40085,#8310,#8311);
#6865=AXIS2_PLACEMENT_3D('',#40087,#8313,#8314);
#6866=AXIS2_PLACEMENT_3D('',#40090,#8315,#8316);
#6867=AXIS2_PLACEMENT_3D('',#40091,#8317,#8318);
#6868=AXIS2_PLACEMENT_3D('',#40093,#8320,#8321);
#6869=AXIS2_PLACEMENT_3D('',#40096,#8322,#8323);
#6870=AXIS2_PLACEMENT_3D('',#40097,#8324,#8325);
#6871=AXIS2_PLACEMENT_3D('',#40101,#8327,#8328);
#6872=AXIS2_PLACEMENT_3D('',#40102,#8329,#8330);
#6873=AXIS2_PLACEMENT_3D('',#40103,#8331,#8332);
#6874=AXIS2_PLACEMENT_3D('',#40105,#8334,#8335);
#6875=AXIS2_PLACEMENT_3D('',#40108,#8336,#8337);
#6876=AXIS2_PLACEMENT_3D('',#40109,#8338,#8339);
#6877=AXIS2_PLACEMENT_3D('',#40111,#8341,#8342);
#6878=AXIS2_PLACEMENT_3D('',#40114,#8343,#8344);
#6879=AXIS2_PLACEMENT_3D('',#40115,#8345,#8346);
#6880=AXIS2_PLACEMENT_3D('',#40119,#8348,#8349);
#6881=AXIS2_PLACEMENT_3D('',#40120,#8350,#8351);
#6882=AXIS2_PLACEMENT_3D('',#40121,#8352,#8353);
#6883=AXIS2_PLACEMENT_3D('',#40123,#8355,#8356);
#6884=AXIS2_PLACEMENT_3D('',#40126,#8357,#8358);
#6885=AXIS2_PLACEMENT_3D('',#40127,#8359,#8360);
#6886=AXIS2_PLACEMENT_3D('',#40129,#8362,#8363);
#6887=AXIS2_PLACEMENT_3D('',#40132,#8364,#8365);
#6888=AXIS2_PLACEMENT_3D('',#40133,#8366,#8367);
#6889=AXIS2_PLACEMENT_3D('',#40137,#8369,#8370);
#6890=AXIS2_PLACEMENT_3D('',#40138,#8371,#8372);
#6891=AXIS2_PLACEMENT_3D('',#40139,#8373,#8374);
#6892=AXIS2_PLACEMENT_3D('',#40141,#8376,#8377);
#6893=AXIS2_PLACEMENT_3D('',#40144,#8378,#8379);
#6894=AXIS2_PLACEMENT_3D('',#40145,#8380,#8381);
#6895=AXIS2_PLACEMENT_3D('',#40147,#8383,#8384);
#6896=AXIS2_PLACEMENT_3D('',#40150,#8385,#8386);
#6897=AXIS2_PLACEMENT_3D('',#40151,#8387,#8388);
#6898=AXIS2_PLACEMENT_3D('',#40155,#8390,#8391);
#6899=AXIS2_PLACEMENT_3D('',#40156,#8392,#8393);
#6900=AXIS2_PLACEMENT_3D('',#40157,#8394,#8395);
#6901=AXIS2_PLACEMENT_3D('',#40159,#8397,#8398);
#6902=AXIS2_PLACEMENT_3D('',#40162,#8399,#8400);
#6903=AXIS2_PLACEMENT_3D('',#40163,#8401,#8402);
#6904=AXIS2_PLACEMENT_3D('',#40165,#8404,#8405);
#6905=AXIS2_PLACEMENT_3D('',#40168,#8406,#8407);
#6906=AXIS2_PLACEMENT_3D('',#40169,#8408,#8409);
#6907=AXIS2_PLACEMENT_3D('',#40173,#8411,#8412);
#6908=AXIS2_PLACEMENT_3D('',#40174,#8413,#8414);
#6909=AXIS2_PLACEMENT_3D('',#40175,#8415,#8416);
#6910=AXIS2_PLACEMENT_3D('',#40177,#8418,#8419);
#6911=AXIS2_PLACEMENT_3D('',#40180,#8420,#8421);
#6912=AXIS2_PLACEMENT_3D('',#40181,#8422,#8423);
#6913=AXIS2_PLACEMENT_3D('',#40183,#8425,#8426);
#6914=AXIS2_PLACEMENT_3D('',#40186,#8427,#8428);
#6915=AXIS2_PLACEMENT_3D('',#40187,#8429,#8430);
#6916=AXIS2_PLACEMENT_3D('',#40191,#8432,#8433);
#6917=AXIS2_PLACEMENT_3D('',#40192,#8434,#8435);
#6918=AXIS2_PLACEMENT_3D('',#40193,#8436,#8437);
#6919=AXIS2_PLACEMENT_3D('',#40195,#8439,#8440);
#6920=AXIS2_PLACEMENT_3D('',#40198,#8441,#8442);
#6921=AXIS2_PLACEMENT_3D('',#40199,#8443,#8444);
#6922=AXIS2_PLACEMENT_3D('',#40201,#8446,#8447);
#6923=AXIS2_PLACEMENT_3D('',#40204,#8448,#8449);
#6924=AXIS2_PLACEMENT_3D('',#40205,#8450,#8451);
#6925=AXIS2_PLACEMENT_3D('',#40209,#8453,#8454);
#6926=AXIS2_PLACEMENT_3D('',#40210,#8455,#8456);
#6927=AXIS2_PLACEMENT_3D('',#40211,#8457,#8458);
#6928=AXIS2_PLACEMENT_3D('',#40213,#8460,#8461);
#6929=AXIS2_PLACEMENT_3D('',#40216,#8462,#8463);
#6930=AXIS2_PLACEMENT_3D('',#40217,#8464,#8465);
#6931=AXIS2_PLACEMENT_3D('',#40219,#8467,#8468);
#6932=AXIS2_PLACEMENT_3D('',#40222,#8469,#8470);
#6933=AXIS2_PLACEMENT_3D('',#40223,#8471,#8472);
#6934=AXIS2_PLACEMENT_3D('',#40227,#8474,#8475);
#6935=AXIS2_PLACEMENT_3D('',#40228,#8476,#8477);
#6936=AXIS2_PLACEMENT_3D('',#40229,#8478,#8479);
#6937=AXIS2_PLACEMENT_3D('',#40231,#8481,#8482);
#6938=AXIS2_PLACEMENT_3D('',#40234,#8483,#8484);
#6939=AXIS2_PLACEMENT_3D('',#40235,#8485,#8486);
#6940=AXIS2_PLACEMENT_3D('',#40237,#8488,#8489);
#6941=AXIS2_PLACEMENT_3D('',#40240,#8490,#8491);
#6942=AXIS2_PLACEMENT_3D('',#40241,#8492,#8493);
#6943=AXIS2_PLACEMENT_3D('',#40245,#8495,#8496);
#6944=AXIS2_PLACEMENT_3D('',#40246,#8497,#8498);
#6945=AXIS2_PLACEMENT_3D('',#40247,#8499,#8500);
#6946=AXIS2_PLACEMENT_3D('',#40249,#8502,#8503);
#6947=AXIS2_PLACEMENT_3D('',#40252,#8504,#8505);
#6948=AXIS2_PLACEMENT_3D('',#40253,#8506,#8507);
#6949=AXIS2_PLACEMENT_3D('',#40255,#8509,#8510);
#6950=AXIS2_PLACEMENT_3D('',#40258,#8511,#8512);
#6951=AXIS2_PLACEMENT_3D('',#40259,#8513,#8514);
#6952=AXIS2_PLACEMENT_3D('',#40263,#8516,#8517);
#6953=AXIS2_PLACEMENT_3D('',#40264,#8518,#8519);
#6954=AXIS2_PLACEMENT_3D('',#40265,#8520,#8521);
#6955=AXIS2_PLACEMENT_3D('',#40267,#8523,#8524);
#6956=AXIS2_PLACEMENT_3D('',#40270,#8525,#8526);
#6957=AXIS2_PLACEMENT_3D('',#40271,#8527,#8528);
#6958=AXIS2_PLACEMENT_3D('',#40273,#8530,#8531);
#6959=AXIS2_PLACEMENT_3D('',#40276,#8532,#8533);
#6960=AXIS2_PLACEMENT_3D('',#40277,#8534,#8535);
#6961=AXIS2_PLACEMENT_3D('',#40281,#8537,#8538);
#6962=AXIS2_PLACEMENT_3D('',#40282,#8539,#8540);
#6963=AXIS2_PLACEMENT_3D('',#40283,#8541,#8542);
#6964=AXIS2_PLACEMENT_3D('',#40285,#8544,#8545);
#6965=AXIS2_PLACEMENT_3D('',#40288,#8546,#8547);
#6966=AXIS2_PLACEMENT_3D('',#40289,#8548,#8549);
#6967=AXIS2_PLACEMENT_3D('',#40291,#8551,#8552);
#6968=AXIS2_PLACEMENT_3D('',#40294,#8553,#8554);
#6969=AXIS2_PLACEMENT_3D('',#40295,#8555,#8556);
#6970=AXIS2_PLACEMENT_3D('',#40299,#8558,#8559);
#6971=AXIS2_PLACEMENT_3D('',#40300,#8560,#8561);
#6972=AXIS2_PLACEMENT_3D('',#40301,#8562,#8563);
#6973=AXIS2_PLACEMENT_3D('',#40303,#8565,#8566);
#6974=AXIS2_PLACEMENT_3D('',#40306,#8567,#8568);
#6975=AXIS2_PLACEMENT_3D('',#40307,#8569,#8570);
#6976=AXIS2_PLACEMENT_3D('',#40309,#8571,#8572);
#6977=AXIS2_PLACEMENT_3D('',#40310,#8573,#8574);
#6978=AXIS2_PLACEMENT_3D('',#40311,#8575,#8576);
#6979=AXIS2_PLACEMENT_3D('',#40314,#8577,#8578);
#6980=AXIS2_PLACEMENT_3D('',#40316,#8579,#8580);
#6981=AXIS2_PLACEMENT_3D('',#40318,#8581,#8582);
#6982=AXIS2_PLACEMENT_3D('',#40321,#8584,#8585);
#6983=AXIS2_PLACEMENT_3D('',#40323,#8586,#8587);
#6984=AXIS2_PLACEMENT_3D('',#40325,#8588,#8589);
#6985=AXIS2_PLACEMENT_3D('',#40326,#8590,#8591);
#6986=AXIS2_PLACEMENT_3D('',#40327,#8592,#8593);
#6987=AXIS2_PLACEMENT_3D('',#40329,#8595,#8596);
#6988=AXIS2_PLACEMENT_3D('',#40330,#8597,#8598);
#6989=AXIS2_PLACEMENT_3D('',#40334,#8601,#8602);
#6990=AXIS2_PLACEMENT_3D('',#40338,#8605,#8606);
#6991=AXIS2_PLACEMENT_3D('',#40342,#8609,#8610);
#6992=AXIS2_PLACEMENT_3D('',#40346,#8613,#8614);
#6993=AXIS2_PLACEMENT_3D('',#40350,#8617,#8618);
#6994=AXIS2_PLACEMENT_3D('',#40354,#8621,#8622);
#6995=AXIS2_PLACEMENT_3D('',#40357,#8623,#8624);
#6996=AXIS2_PLACEMENT_3D('',#40359,#8625,#8626);
#6997=AXIS2_PLACEMENT_3D('',#40361,#8627,#8628);
#6998=AXIS2_PLACEMENT_3D('',#40363,#8629,#8630);
#6999=AXIS2_PLACEMENT_3D('',#40365,#8631,#8632);
#7000=AXIS2_PLACEMENT_3D('',#40366,#8633,#8634);
#7001=AXIS2_PLACEMENT_3D('',#40367,#8635,#8636);
#7002=AXIS2_PLACEMENT_3D('',#40375,#8637,#8638);
#7003=AXIS2_PLACEMENT_3D('',#40383,#8639,#8640);
#7004=AXIS2_PLACEMENT_3D('',#40391,#8641,#8642);
#7005=AXIS2_PLACEMENT_3D('',#40399,#8643,#8644);
#7006=AXIS2_PLACEMENT_3D('',#40407,#8645,#8646);
#7007=AXIS2_PLACEMENT_3D('',#40415,#8647,#8648);
#7008=AXIS2_PLACEMENT_3D('',#40418,#8651,#8652);
#7009=AXIS2_PLACEMENT_3D('',#40420,#8654,#8655);
#7010=AXIS2_PLACEMENT_3D('',#40422,#8657,#8658);
#7011=AXIS2_PLACEMENT_3D('',#40424,#8660,#8661);
#7012=AXIS2_PLACEMENT_3D('',#40426,#8663,#8664);
#7013=AXIS2_PLACEMENT_3D('',#40427,#8665,#8666);
#8246=DIRECTION('axis',(0.,0.,1.));
#8247=DIRECTION('refdir',(1.,0.,0.));
#8248=DIRECTION('center_axis',(-1.,0.,0.));
#8249=DIRECTION('ref_axis',(0.,0.,1.));
#8250=DIRECTION('center_axis',(1.,1.22460635382238E-16,0.));
#8251=DIRECTION('ref_axis',(-1.22460635382238E-16,1.,0.));
#8252=DIRECTION('center_axis',(1.,1.22460635382238E-16,0.));
#8253=DIRECTION('ref_axis',(-1.22460635382238E-16,1.,0.));
#8254=DIRECTION('',(0.707106781186552,8.65956056235487E-17,0.707106781186543));
#8255=DIRECTION('center_axis',(-1.,0.,0.));
#8256=DIRECTION('ref_axis',(0.,0.,1.));
#8257=DIRECTION('center_axis',(-1.,-1.22460635382238E-16,0.));
#8258=DIRECTION('ref_axis',(1.22460635382238E-16,-1.,0.));
#8259=DIRECTION('center_axis',(-1.,-1.22460635382238E-16,0.));
#8260=DIRECTION('ref_axis',(1.22460635382238E-16,-1.,0.));
#8261=DIRECTION('center_axis',(-1.,-1.22460635382238E-16,0.));
#8262=DIRECTION('ref_axis',(1.22460635382238E-16,-1.,0.));
#8263=DIRECTION('',(0.57357643635105,-0.819152044288989,1.00317192905352E-16));
#8264=DIRECTION('center_axis',(-1.,-1.22460635382238E-16,0.));
#8265=DIRECTION('ref_axis',(1.22460635382238E-16,-1.,0.));
#8266=DIRECTION('center_axis',(-1.,-1.22460635382238E-16,0.));
#8267=DIRECTION('ref_axis',(1.22460635382238E-16,-1.,0.));
#8268=DIRECTION('center_axis',(1.,1.22460635382238E-16,0.));
#8269=DIRECTION('ref_axis',(-1.22460635382238E-16,1.,0.));
#8270=DIRECTION('',(-0.573576436351045,0.819152044288993,1.00317192905353E-16));
#8271=DIRECTION('center_axis',(-1.,0.,0.));
#8272=DIRECTION('ref_axis',(0.,0.,1.));
#8273=DIRECTION('center_axis',(-1.,-1.22460635382238E-16,0.));
#8274=DIRECTION('ref_axis',(1.22460635382238E-16,-1.,0.));
#8275=DIRECTION('center_axis',(-1.,-1.22460635382238E-16,0.));
#8276=DIRECTION('ref_axis',(1.22460635382238E-16,-1.,0.));
#8277=DIRECTION('',(1.,0.,0.));
#8278=DIRECTION('center_axis',(-1.,-1.22460635382238E-16,0.));
#8279=DIRECTION('ref_axis',(1.22460635382238E-16,-1.,0.));
#8280=DIRECTION('center_axis',(-1.,-1.22460635382238E-16,0.));
#8281=DIRECTION('ref_axis',(1.22460635382238E-16,-1.,0.));
#8282=DIRECTION('center_axis',(-1.,-1.22460635382238E-16,0.));
#8283=DIRECTION('ref_axis',(1.22460635382238E-16,-1.,0.));
#8284=DIRECTION('',(0.57357643635105,-0.819152044288989,1.00317192905352E-16));
#8285=DIRECTION('center_axis',(-1.,-1.22460635382238E-16,0.));
#8286=DIRECTION('ref_axis',(1.22460635382238E-16,-1.,0.));
#8287=DIRECTION('center_axis',(-1.,-1.22460635382238E-16,0.));
#8288=DIRECTION('ref_axis',(1.22460635382238E-16,-1.,0.));
#8289=DIRECTION('center_axis',(1.,1.22460635382238E-16,0.));
#8290=DIRECTION('ref_axis',(-1.22460635382238E-16,1.,0.));
#8291=DIRECTION('',(-0.573576436351045,0.819152044288993,1.00317192905353E-16));
#8292=DIRECTION('center_axis',(-1.,0.,0.));
#8293=DIRECTION('ref_axis',(0.,0.,1.));
#8294=DIRECTION('center_axis',(-1.,-1.22460635382238E-16,0.));
#8295=DIRECTION('ref_axis',(1.22460635382238E-16,-1.,0.));
#8296=DIRECTION('center_axis',(-1.,-1.22460635382238E-16,0.));
#8297=DIRECTION('ref_axis',(1.22460635382238E-16,-1.,0.));
#8298=DIRECTION('',(1.,0.,0.));
#8299=DIRECTION('center_axis',(-1.,-1.22460635382238E-16,0.));
#8300=DIRECTION('ref_axis',(1.22460635382238E-16,-1.,0.));
#8301=DIRECTION('center_axis',(-1.,-1.22460635382238E-16,0.));
#8302=DIRECTION('ref_axis',(1.22460635382238E-16,-1.,0.));
#8303=DIRECTION('center_axis',(-1.,-1.22460635382238E-16,0.));
#8304=DIRECTION('ref_axis',(1.22460635382238E-16,-1.,0.));
#8305=DIRECTION('',(0.57357643635105,-0.819152044288989,1.00317192905352E-16));
#8306=DIRECTION('center_axis',(-1.,-1.22460635382238E-16,0.));
#8307=DIRECTION('ref_axis',(1.22460635382238E-16,-1.,0.));
#8308=DIRECTION('center_axis',(-1.,-1.22460635382238E-16,0.));
#8309=DIRECTION('ref_axis',(1.22460635382238E-16,-1.,0.));
#8310=DIRECTION('center_axis',(1.,1.22460635382238E-16,0.));
#8311=DIRECTION('ref_axis',(-1.22460635382238E-16,1.,0.));
#8312=DIRECTION('',(-0.573576436351045,0.819152044288993,1.00317192905353E-16));
#8313=DIRECTION('center_axis',(-1.,0.,0.));
#8314=DIRECTION('ref_axis',(0.,0.,1.));
#8315=DIRECTION('center_axis',(-1.,-1.22460635382238E-16,0.));
#8316=DIRECTION('ref_axis',(1.22460635382238E-16,-1.,0.));
#8317=DIRECTION('center_axis',(-1.,-1.22460635382238E-16,0.));
#8318=DIRECTION('ref_axis',(1.22460635382238E-16,-1.,0.));
#8319=DIRECTION('',(1.,0.,0.));
#8320=DIRECTION('center_axis',(-1.,-1.22460635382238E-16,0.));
#8321=DIRECTION('ref_axis',(1.22460635382238E-16,-1.,0.));
#8322=DIRECTION('center_axis',(-1.,-1.22460635382238E-16,0.));
#8323=DIRECTION('ref_axis',(1.22460635382238E-16,-1.,0.));
#8324=DIRECTION('center_axis',(-1.,-1.22460635382238E-16,0.));
#8325=DIRECTION('ref_axis',(1.22460635382238E-16,-1.,0.));
#8326=DIRECTION('',(0.57357643635105,-0.819152044288989,1.00317192905352E-16));
#8327=DIRECTION('center_axis',(-1.,-1.22460635382238E-16,0.));
#8328=DIRECTION('ref_axis',(1.22460635382238E-16,-1.,0.));
#8329=DIRECTION('center_axis',(-1.,-1.22460635382238E-16,0.));
#8330=DIRECTION('ref_axis',(1.22460635382238E-16,-1.,0.));
#8331=DIRECTION('center_axis',(1.,1.22460635382238E-16,0.));
#8332=DIRECTION('ref_axis',(-1.22460635382238E-16,1.,0.));
#8333=DIRECTION('',(-0.573576436351045,0.819152044288993,1.00317192905353E-16));
#8334=DIRECTION('center_axis',(-1.,0.,0.));
#8335=DIRECTION('ref_axis',(0.,0.,1.));
#8336=DIRECTION('center_axis',(-1.,-1.22460635382238E-16,0.));
#8337=DIRECTION('ref_axis',(1.22460635382238E-16,-1.,0.));
#8338=DIRECTION('center_axis',(-1.,-1.22460635382238E-16,0.));
#8339=DIRECTION('ref_axis',(1.22460635382238E-16,-1.,0.));
#8340=DIRECTION('',(1.,0.,0.));
#8341=DIRECTION('center_axis',(-1.,-1.22460635382238E-16,0.));
#8342=DIRECTION('ref_axis',(1.22460635382238E-16,-1.,0.));
#8343=DIRECTION('center_axis',(-1.,-1.22460635382238E-16,0.));
#8344=DIRECTION('ref_axis',(1.22460635382238E-16,-1.,0.));
#8345=DIRECTION('center_axis',(-1.,-1.22460635382238E-16,0.));
#8346=DIRECTION('ref_axis',(1.22460635382238E-16,-1.,0.));
#8347=DIRECTION('',(0.57357643635105,-0.819152044288989,1.00317192905352E-16));
#8348=DIRECTION('center_axis',(-1.,-1.22460635382238E-16,0.));
#8349=DIRECTION('ref_axis',(1.22460635382238E-16,-1.,0.));
#8350=DIRECTION('center_axis',(-1.,-1.22460635382238E-16,0.));
#8351=DIRECTION('ref_axis',(1.22460635382238E-16,-1.,0.));
#8352=DIRECTION('center_axis',(1.,1.22460635382238E-16,0.));
#8353=DIRECTION('ref_axis',(-1.22460635382238E-16,1.,0.));
#8354=DIRECTION('',(-0.573576436351045,0.819152044288993,1.00317192905353E-16));
#8355=DIRECTION('center_axis',(-1.,0.,0.));
#8356=DIRECTION('ref_axis',(0.,0.,1.));
#8357=DIRECTION('center_axis',(-1.,-1.22460635382238E-16,0.));
#8358=DIRECTION('ref_axis',(1.22460635382238E-16,-1.,0.));
#8359=DIRECTION('center_axis',(-1.,-1.22460635382238E-16,0.));
#8360=DIRECTION('ref_axis',(1.22460635382238E-16,-1.,0.));
#8361=DIRECTION('',(1.,0.,0.));
#8362=DIRECTION('center_axis',(-1.,-1.22460635382238E-16,0.));
#8363=DIRECTION('ref_axis',(1.22460635382238E-16,-1.,0.));
#8364=DIRECTION('center_axis',(-1.,-1.22460635382238E-16,0.));
#8365=DIRECTION('ref_axis',(1.22460635382238E-16,-1.,0.));
#8366=DIRECTION('center_axis',(-1.,-1.22460635382238E-16,0.));
#8367=DIRECTION('ref_axis',(1.22460635382238E-16,-1.,0.));
#8368=DIRECTION('',(0.57357643635105,-0.819152044288989,1.00317192905352E-16));
#8369=DIRECTION('center_axis',(-1.,-1.22460635382238E-16,0.));
#8370=DIRECTION('ref_axis',(1.22460635382238E-16,-1.,0.));
#8371=DIRECTION('center_axis',(-1.,-1.22460635382238E-16,0.));
#8372=DIRECTION('ref_axis',(1.22460635382238E-16,-1.,0.));
#8373=DIRECTION('center_axis',(1.,1.22460635382238E-16,0.));
#8374=DIRECTION('ref_axis',(-1.22460635382238E-16,1.,0.));
#8375=DIRECTION('',(-0.573576436351045,0.819152044288993,1.00317192905353E-16));
#8376=DIRECTION('center_axis',(-1.,0.,0.));
#8377=DIRECTION('ref_axis',(0.,0.,1.));
#8378=DIRECTION('center_axis',(-1.,-1.22460635382238E-16,0.));
#8379=DIRECTION('ref_axis',(1.22460635382238E-16,-1.,0.));
#8380=DIRECTION('center_axis',(-1.,-1.22460635382238E-16,0.));
#8381=DIRECTION('ref_axis',(1.22460635382238E-16,-1.,0.));
#8382=DIRECTION('',(1.,0.,0.));
#8383=DIRECTION('center_axis',(-1.,-1.22460635382238E-16,0.));
#8384=DIRECTION('ref_axis',(1.22460635382238E-16,-1.,0.));
#8385=DIRECTION('center_axis',(-1.,-1.22460635382238E-16,0.));
#8386=DIRECTION('ref_axis',(1.22460635382238E-16,-1.,0.));
#8387=DIRECTION('center_axis',(-1.,-1.22460635382238E-16,0.));
#8388=DIRECTION('ref_axis',(1.22460635382238E-16,-1.,0.));
#8389=DIRECTION('',(0.57357643635105,-0.819152044288989,1.00317192905352E-16));
#8390=DIRECTION('center_axis',(-1.,-1.22460635382238E-16,0.));
#8391=DIRECTION('ref_axis',(1.22460635382238E-16,-1.,0.));
#8392=DIRECTION('center_axis',(-1.,-1.22460635382238E-16,0.));
#8393=DIRECTION('ref_axis',(1.22460635382238E-16,-1.,0.));
#8394=DIRECTION('center_axis',(1.,1.22460635382238E-16,0.));
#8395=DIRECTION('ref_axis',(-1.22460635382238E-16,1.,0.));
#8396=DIRECTION('',(-0.573576436351045,0.819152044288993,1.00317192905353E-16));
#8397=DIRECTION('center_axis',(-1.,0.,0.));
#8398=DIRECTION('ref_axis',(0.,0.,1.));
#8399=DIRECTION('center_axis',(-1.,-1.22460635382238E-16,0.));
#8400=DIRECTION('ref_axis',(1.22460635382238E-16,-1.,0.));
#8401=DIRECTION('center_axis',(-1.,-1.22460635382238E-16,0.));
#8402=DIRECTION('ref_axis',(1.22460635382238E-16,-1.,0.));
#8403=DIRECTION('',(1.,0.,0.));
#8404=DIRECTION('center_axis',(-1.,-1.22460635382238E-16,0.));
#8405=DIRECTION('ref_axis',(1.22460635382238E-16,-1.,0.));
#8406=DIRECTION('center_axis',(-1.,-1.22460635382238E-16,0.));
#8407=DIRECTION('ref_axis',(1.22460635382238E-16,-1.,0.));
#8408=DIRECTION('center_axis',(-1.,-1.22460635382238E-16,0.));
#8409=DIRECTION('ref_axis',(1.22460635382238E-16,-1.,0.));
#8410=DIRECTION('',(0.57357643635105,-0.819152044288989,1.00317192905352E-16));
#8411=DIRECTION('center_axis',(-1.,-1.22460635382238E-16,0.));
#8412=DIRECTION('ref_axis',(1.22460635382238E-16,-1.,0.));
#8413=DIRECTION('center_axis',(-1.,-1.22460635382238E-16,0.));
#8414=DIRECTION('ref_axis',(1.22460635382238E-16,-1.,0.));
#8415=DIRECTION('center_axis',(1.,1.22460635382238E-16,0.));
#8416=DIRECTION('ref_axis',(-1.22460635382238E-16,1.,0.));
#8417=DIRECTION('',(-0.573576436351045,0.819152044288993,1.00317192905353E-16));
#8418=DIRECTION('center_axis',(-1.,0.,0.));
#8419=DIRECTION('ref_axis',(0.,0.,1.));
#8420=DIRECTION('center_axis',(-1.,-1.22460635382238E-16,0.));
#8421=DIRECTION('ref_axis',(1.22460635382238E-16,-1.,0.));
#8422=DIRECTION('center_axis',(-1.,-1.22460635382238E-16,0.));
#8423=DIRECTION('ref_axis',(1.22460635382238E-16,-1.,0.));
#8424=DIRECTION('',(1.,0.,0.));
#8425=DIRECTION('center_axis',(-1.,-1.22460635382238E-16,0.));
#8426=DIRECTION('ref_axis',(1.22460635382238E-16,-1.,0.));
#8427=DIRECTION('center_axis',(-1.,-1.22460635382238E-16,0.));
#8428=DIRECTION('ref_axis',(1.22460635382238E-16,-1.,0.));
#8429=DIRECTION('center_axis',(-1.,-1.22460635382238E-16,0.));
#8430=DIRECTION('ref_axis',(1.22460635382238E-16,-1.,0.));
#8431=DIRECTION('',(0.57357643635105,-0.819152044288989,1.00317192905352E-16));
#8432=DIRECTION('center_axis',(-1.,-1.22460635382238E-16,0.));
#8433=DIRECTION('ref_axis',(1.22460635382238E-16,-1.,0.));
#8434=DIRECTION('center_axis',(-1.,-1.22460635382238E-16,0.));
#8435=DIRECTION('ref_axis',(1.22460635382238E-16,-1.,0.));
#8436=DIRECTION('center_axis',(1.,1.22460635382238E-16,0.));
#8437=DIRECTION('ref_axis',(-1.22460635382238E-16,1.,0.));
#8438=DIRECTION('',(-0.573576436351045,0.819152044288993,1.00317192905353E-16));
#8439=DIRECTION('center_axis',(-1.,0.,0.));
#8440=DIRECTION('ref_axis',(0.,0.,1.));
#8441=DIRECTION('center_axis',(-1.,-1.22460635382238E-16,0.));
#8442=DIRECTION('ref_axis',(1.22460635382238E-16,-1.,0.));
#8443=DIRECTION('center_axis',(-1.,-1.22460635382238E-16,0.));
#8444=DIRECTION('ref_axis',(1.22460635382238E-16,-1.,0.));
#8445=DIRECTION('',(1.,0.,0.));
#8446=DIRECTION('center_axis',(-1.,-1.22460635382238E-16,0.));
#8447=DIRECTION('ref_axis',(1.22460635382238E-16,-1.,0.));
#8448=DIRECTION('center_axis',(-1.,-1.22460635382238E-16,0.));
#8449=DIRECTION('ref_axis',(1.22460635382238E-16,-1.,0.));
#8450=DIRECTION('center_axis',(-1.,-1.22460635382238E-16,0.));
#8451=DIRECTION('ref_axis',(1.22460635382238E-16,-1.,0.));
#8452=DIRECTION('',(0.57357643635105,-0.819152044288989,1.00317192905352E-16));
#8453=DIRECTION('center_axis',(-1.,-1.22460635382238E-16,0.));
#8454=DIRECTION('ref_axis',(1.22460635382238E-16,-1.,0.));
#8455=DIRECTION('center_axis',(-1.,-1.22460635382238E-16,0.));
#8456=DIRECTION('ref_axis',(1.22460635382238E-16,-1.,0.));
#8457=DIRECTION('center_axis',(1.,1.22460635382238E-16,0.));
#8458=DIRECTION('ref_axis',(-1.22460635382238E-16,1.,0.));
#8459=DIRECTION('',(-0.573576436351045,0.819152044288993,1.00317192905353E-16));
#8460=DIRECTION('center_axis',(-1.,0.,0.));
#8461=DIRECTION('ref_axis',(0.,0.,1.));
#8462=DIRECTION('center_axis',(-1.,-1.22460635382238E-16,0.));
#8463=DIRECTION('ref_axis',(1.22460635382238E-16,-1.,0.));
#8464=DIRECTION('center_axis',(-1.,-1.22460635382238E-16,0.));
#8465=DIRECTION('ref_axis',(1.22460635382238E-16,-1.,0.));
#8466=DIRECTION('',(1.,0.,0.));
#8467=DIRECTION('center_axis',(-1.,-1.22460635382238E-16,0.));
#8468=DIRECTION('ref_axis',(1.22460635382238E-16,-1.,0.));
#8469=DIRECTION('center_axis',(-1.,-1.22460635382238E-16,0.));
#8470=DIRECTION('ref_axis',(1.22460635382238E-16,-1.,0.));
#8471=DIRECTION('center_axis',(-1.,-1.22460635382238E-16,0.));
#8472=DIRECTION('ref_axis',(1.22460635382238E-16,-1.,0.));
#8473=DIRECTION('',(0.57357643635105,-0.819152044288989,1.00317192905352E-16));
#8474=DIRECTION('center_axis',(-1.,-1.22460635382238E-16,0.));
#8475=DIRECTION('ref_axis',(1.22460635382238E-16,-1.,0.));
#8476=DIRECTION('center_axis',(-1.,-1.22460635382238E-16,0.));
#8477=DIRECTION('ref_axis',(1.22460635382238E-16,-1.,0.));
#8478=DIRECTION('center_axis',(1.,1.22460635382238E-16,0.));
#8479=DIRECTION('ref_axis',(-1.22460635382238E-16,1.,0.));
#8480=DIRECTION('',(-0.573576436351045,0.819152044288993,1.00317192905353E-16));
#8481=DIRECTION('center_axis',(-1.,0.,0.));
#8482=DIRECTION('ref_axis',(0.,0.,1.));
#8483=DIRECTION('center_axis',(-1.,-1.22460635382238E-16,0.));
#8484=DIRECTION('ref_axis',(1.22460635382238E-16,-1.,0.));
#8485=DIRECTION('center_axis',(-1.,-1.22460635382238E-16,0.));
#8486=DIRECTION('ref_axis',(1.22460635382238E-16,-1.,0.));
#8487=DIRECTION('',(1.,0.,0.));
#8488=DIRECTION('center_axis',(-1.,-1.22460635382238E-16,0.));
#8489=DIRECTION('ref_axis',(1.22460635382238E-16,-1.,0.));
#8490=DIRECTION('center_axis',(-1.,-1.22460635382238E-16,0.));
#8491=DIRECTION('ref_axis',(1.22460635382238E-16,-1.,0.));
#8492=DIRECTION('center_axis',(-1.,-1.22460635382238E-16,0.));
#8493=DIRECTION('ref_axis',(1.22460635382238E-16,-1.,0.));
#8494=DIRECTION('',(0.57357643635105,-0.819152044288989,1.00317192905352E-16));
#8495=DIRECTION('center_axis',(-1.,-1.22460635382238E-16,0.));
#8496=DIRECTION('ref_axis',(1.22460635382238E-16,-1.,0.));
#8497=DIRECTION('center_axis',(-1.,-1.22460635382238E-16,0.));
#8498=DIRECTION('ref_axis',(1.22460635382238E-16,-1.,0.));
#8499=DIRECTION('center_axis',(1.,1.22460635382238E-16,0.));
#8500=DIRECTION('ref_axis',(-1.22460635382238E-16,1.,0.));
#8501=DIRECTION('',(-0.573576436351045,0.819152044288993,1.00317192905353E-16));
#8502=DIRECTION('center_axis',(-1.,0.,0.));
#8503=DIRECTION('ref_axis',(0.,0.,1.));
#8504=DIRECTION('center_axis',(-1.,-1.22460635382238E-16,0.));
#8505=DIRECTION('ref_axis',(1.22460635382238E-16,-1.,0.));
#8506=DIRECTION('center_axis',(-1.,-1.22460635382238E-16,0.));
#8507=DIRECTION('ref_axis',(1.22460635382238E-16,-1.,0.));
#8508=DIRECTION('',(1.,0.,0.));
#8509=DIRECTION('center_axis',(-1.,-1.22460635382238E-16,0.));
#8510=DIRECTION('ref_axis',(1.22460635382238E-16,-1.,0.));
#8511=DIRECTION('center_axis',(-1.,-1.22460635382238E-16,0.));
#8512=DIRECTION('ref_axis',(1.22460635382238E-16,-1.,0.));
#8513=DIRECTION('center_axis',(-1.,-1.22460635382238E-16,0.));
#8514=DIRECTION('ref_axis',(1.22460635382238E-16,-1.,0.));
#8515=DIRECTION('',(0.57357643635105,-0.819152044288989,1.00317192905352E-16));
#8516=DIRECTION('center_axis',(-1.,-1.22460635382238E-16,0.));
#8517=DIRECTION('ref_axis',(1.22460635382238E-16,-1.,0.));
#8518=DIRECTION('center_axis',(-1.,-1.22460635382238E-16,0.));
#8519=DIRECTION('ref_axis',(1.22460635382238E-16,-1.,0.));
#8520=DIRECTION('center_axis',(1.,1.22460635382238E-16,0.));
#8521=DIRECTION('ref_axis',(-1.22460635382238E-16,1.,0.));
#8522=DIRECTION('',(-0.573576436351045,0.819152044288993,1.00317192905353E-16));
#8523=DIRECTION('center_axis',(-1.,0.,0.));
#8524=DIRECTION('ref_axis',(0.,0.,1.));
#8525=DIRECTION('center_axis',(-1.,-1.22460635382238E-16,0.));
#8526=DIRECTION('ref_axis',(1.22460635382238E-16,-1.,0.));
#8527=DIRECTION('center_axis',(-1.,-1.22460635382238E-16,0.));
#8528=DIRECTION('ref_axis',(1.22460635382238E-16,-1.,0.));
#8529=DIRECTION('',(1.,0.,0.));
#8530=DIRECTION('center_axis',(-1.,-1.22460635382238E-16,0.));
#8531=DIRECTION('ref_axis',(1.22460635382238E-16,-1.,0.));
#8532=DIRECTION('center_axis',(-1.,-1.22460635382238E-16,0.));
#8533=DIRECTION('ref_axis',(1.22460635382238E-16,-1.,0.));
#8534=DIRECTION('center_axis',(-1.,-1.22460635382238E-16,0.));
#8535=DIRECTION('ref_axis',(1.22460635382238E-16,-1.,0.));
#8536=DIRECTION('',(0.57357643635105,-0.819152044288989,1.00317192905352E-16));
#8537=DIRECTION('center_axis',(-1.,-1.22460635382238E-16,0.));
#8538=DIRECTION('ref_axis',(1.22460635382238E-16,-1.,0.));
#8539=DIRECTION('center_axis',(-1.,-1.22460635382238E-16,0.));
#8540=DIRECTION('ref_axis',(1.22460635382238E-16,-1.,0.));
#8541=DIRECTION('center_axis',(1.,1.22460635382238E-16,0.));
#8542=DIRECTION('ref_axis',(-1.22460635382238E-16,1.,0.));
#8543=DIRECTION('',(-0.573576436351045,0.819152044288993,1.00317192905353E-16));
#8544=DIRECTION('center_axis',(-1.,0.,0.));
#8545=DIRECTION('ref_axis',(0.,0.,1.));
#8546=DIRECTION('center_axis',(-1.,-1.22460635382238E-16,0.));
#8547=DIRECTION('ref_axis',(1.22460635382238E-16,-1.,0.));
#8548=DIRECTION('center_axis',(-1.,-1.22460635382238E-16,0.));
#8549=DIRECTION('ref_axis',(1.22460635382238E-16,-1.,0.));
#8550=DIRECTION('',(1.,0.,0.));
#8551=DIRECTION('center_axis',(-1.,-1.22460635382238E-16,0.));
#8552=DIRECTION('ref_axis',(1.22460635382238E-16,-1.,0.));
#8553=DIRECTION('center_axis',(-1.,-1.22460635382238E-16,0.));
#8554=DIRECTION('ref_axis',(1.22460635382238E-16,-1.,0.));
#8555=DIRECTION('center_axis',(-1.,-1.22460635382238E-16,0.));
#8556=DIRECTION('ref_axis',(1.22460635382238E-16,-1.,0.));
#8557=DIRECTION('',(0.57357643635105,-0.819152044288989,1.00317192905352E-16));
#8558=DIRECTION('center_axis',(-1.,-1.22460635382238E-16,0.));
#8559=DIRECTION('ref_axis',(1.22460635382238E-16,-1.,0.));
#8560=DIRECTION('center_axis',(-1.,-1.22460635382238E-16,0.));
#8561=DIRECTION('ref_axis',(1.22460635382238E-16,-1.,0.));
#8562=DIRECTION('center_axis',(1.,1.22460635382238E-16,0.));
#8563=DIRECTION('ref_axis',(-1.22460635382238E-16,1.,0.));
#8564=DIRECTION('',(-0.573576436351045,0.819152044288993,1.00317192905353E-16));
#8565=DIRECTION('center_axis',(1.,0.,0.));
#8566=DIRECTION('ref_axis',(0.,0.,-1.));
#8567=DIRECTION('center_axis',(1.,0.,0.));
#8568=DIRECTION('ref_axis',(0.,0.,-1.));
#8569=DIRECTION('center_axis',(1.,0.,0.));
#8570=DIRECTION('ref_axis',(0.,0.,-1.));
#8571=DIRECTION('center_axis',(0.,1.,1.22464679914735E-16));
#8572=DIRECTION('ref_axis',(0.,-1.22464679914735E-16,1.));
#8573=DIRECTION('center_axis',(-1.,0.,0.));
#8574=DIRECTION('ref_axis',(0.,0.,-1.));
#8575=DIRECTION('center_axis',(-1.,0.,0.));
#8576=DIRECTION('ref_axis',(0.,0.,1.));
#8577=DIRECTION('center_axis',(-1.,0.,0.));
#8578=DIRECTION('ref_axis',(0.,0.,1.));
#8579=DIRECTION('center_axis',(-1.,0.,0.));
#8580=DIRECTION('ref_axis',(0.,0.,1.));
#8581=DIRECTION('center_axis',(-1.,0.,0.));
#8582=DIRECTION('ref_axis',(0.,0.,1.));
#8583=DIRECTION('',(1.,0.,0.));
#8584=DIRECTION('center_axis',(1.,0.,0.));
#8585=DIRECTION('ref_axis',(0.,0.,-1.));
#8586=DIRECTION('center_axis',(-1.,0.,0.));
#8587=DIRECTION('ref_axis',(0.,0.,1.));
#8588=DIRECTION('center_axis',(-1.,0.,0.));
#8589=DIRECTION('ref_axis',(0.,0.,1.));
#8590=DIRECTION('center_axis',(-1.,0.,0.));
#8591=DIRECTION('ref_axis',(0.,0.,1.));
#8592=DIRECTION('center_axis',(-1.,0.,0.));
#8593=DIRECTION('ref_axis',(0.,0.,1.));
#8594=DIRECTION('',(1.,0.,0.));
#8595=DIRECTION('center_axis',(1.,0.,0.));
#8596=DIRECTION('ref_axis',(0.,0.,-1.));
#8597=DIRECTION('center_axis',(1.,0.,0.));
#8598=DIRECTION('ref_axis',(0.,0.,-1.));
#8599=DIRECTION('',(0.,0.500000000000001,0.866025403784438));
#8600=DIRECTION('',(0.,1.,1.35037086860206E-16));
#8601=DIRECTION('center_axis',(1.,0.,0.));
#8602=DIRECTION('ref_axis',(0.,0.,-1.));
#8603=DIRECTION('',(0.,0.500000000000001,0.866025403784438));
#8604=DIRECTION('',(0.,-0.500000000000001,0.866025403784438));
#8605=DIRECTION('center_axis',(1.,0.,0.));
#8606=DIRECTION('ref_axis',(0.,0.,-1.));
#8607=DIRECTION('',(0.,-0.500000000000001,0.866025403784438));
#8608=DIRECTION('',(0.,-1.,1.35037086860206E-16));
#8609=DIRECTION('center_axis',(1.,0.,0.));
#8610=DIRECTION('ref_axis',(0.,0.,-1.));
#8611=DIRECTION('',(0.,-1.,1.35037086860206E-16));
#8612=DIRECTION('',(0.,-0.500000000000002,-0.866025403784437));
#8613=DIRECTION('center_axis',(1.,0.,0.));
#8614=DIRECTION('ref_axis',(0.,0.,-1.));
#8615=DIRECTION('',(0.,-0.500000000000002,-0.866025403784437));
#8616=DIRECTION('',(0.,0.499999999999999,-0.866025403784439));
#8617=DIRECTION('center_axis',(1.,0.,0.));
#8618=DIRECTION('ref_axis',(0.,0.,-1.));
#8619=DIRECTION('',(0.,0.499999999999999,-0.866025403784439));
#8620=DIRECTION('',(0.,1.,1.35037086860206E-16));
#8621=DIRECTION('center_axis',(1.,0.,0.));
#8622=DIRECTION('ref_axis',(0.,0.,-1.));
#8623=DIRECTION('center_axis',(1.,0.,0.));
#8624=DIRECTION('ref_axis',(0.,0.,-1.));
#8625=DIRECTION('center_axis',(1.,0.,0.));
#8626=DIRECTION('ref_axis',(0.,0.,-1.));
#8627=DIRECTION('center_axis',(1.,0.,0.));
#8628=DIRECTION('ref_axis',(0.,0.,-1.));
#8629=DIRECTION('center_axis',(1.,0.,0.));
#8630=DIRECTION('ref_axis',(0.,0.,-1.));
#8631=DIRECTION('center_axis',(-1.,0.,0.));
#8632=DIRECTION('ref_axis',(0.,0.,1.));
#8633=DIRECTION('center_axis',(1.,0.,0.));
#8634=DIRECTION('ref_axis',(0.,0.,-1.));
#8635=DIRECTION('center_axis',(1.,0.,0.));
#8636=DIRECTION('ref_axis',(0.,0.,-1.));
#8637=DIRECTION('center_axis',(1.,0.,0.));
#8638=DIRECTION('ref_axis',(0.,0.,-1.));
#8639=DIRECTION('center_axis',(1.,0.,0.));
#8640=DIRECTION('ref_axis',(0.,0.,-1.));
#8641=DIRECTION('center_axis',(1.,0.,0.));
#8642=DIRECTION('ref_axis',(0.,0.,-1.));
#8643=DIRECTION('center_axis',(1.,0.,0.));
#8644=DIRECTION('ref_axis',(0.,0.,-1.));
#8645=DIRECTION('center_axis',(1.,0.,0.));
#8646=DIRECTION('ref_axis',(0.,0.,-1.));
#8647=DIRECTION('center_axis',(0.,-1.35037086860206E-16,1.));
#8648=DIRECTION('ref_axis',(0.,-1.,-1.35037086860206E-16));
#8649=DIRECTION('',(-1.,0.,0.));
#8650=DIRECTION('',(-1.,0.,0.));
#8651=DIRECTION('center_axis',(0.,0.866025403784439,0.499999999999999));
#8652=DIRECTION('ref_axis',(0.,-0.499999999999999,0.866025403784439));
#8653=DIRECTION('',(-1.,0.,0.));
#8654=DIRECTION('center_axis',(0.,0.866025403784438,-0.500000000000002));
#8655=DIRECTION('ref_axis',(0.,0.500000000000002,0.866025403784437));
#8656=DIRECTION('',(-1.,0.,0.));
#8657=DIRECTION('center_axis',(0.,-1.35037086860206E-16,-1.));
#8658=DIRECTION('ref_axis',(0.,1.,-1.35037086860206E-16));
#8659=DIRECTION('',(-1.,0.,0.));
#8660=DIRECTION('center_axis',(0.,-0.866025403784438,-0.500000000000001));
#8661=DIRECTION('ref_axis',(0.,0.500000000000001,-0.866025403784438));
#8662=DIRECTION('',(-1.,0.,0.));
#8663=DIRECTION('center_axis',(0.,-0.866025403784438,0.500000000000001));
#8664=DIRECTION('ref_axis',(0.,-0.500000000000001,-0.866025403784438));
#8665=DIRECTION('center_axis',(-1.,0.,0.));
#8666=DIRECTION('ref_axis',(0.,0.,1.));
#40030=CARTESIAN_POINT('',(0.,0.,0.));
#40031=CARTESIAN_POINT('Origin',(42.2402,0.,0.));
#40032=CARTESIAN_POINT('',(41.4932323672501,-3.87762075403097E-16,-3.16631763274988));
#40033=CARTESIAN_POINT('',(41.4932323672501,-3.16631763274987,-3.87762075403096E-16));
#40034=CARTESIAN_POINT('Origin',(41.4932323672501,0.,0.));
#40035=CARTESIAN_POINT('Origin',(41.4932323672501,0.,0.));
#40036=CARTESIAN_POINT('',(42.2402,-2.96284923351715E-16,-2.41935));
#40037=CARTESIAN_POINT('',(42.2402,-2.96284923351715E-16,-2.41935));
#40038=CARTESIAN_POINT('Origin',(42.2402,0.,0.));
#40039=CARTESIAN_POINT('Origin',(40.9702,3.22869914397977E-15,0.));
#40040=CARTESIAN_POINT('',(40.4410881737518,-3.88825358729285E-16,-3.175));
#40041=CARTESIAN_POINT('',(40.4410881737518,3.175,-3.88825358729285E-16));
#40042=CARTESIAN_POINT('Origin',(40.4410881737518,3.16390377354917E-15,
0.));
#40043=CARTESIAN_POINT('Origin',(40.4410881737518,3.16390377354917E-15,
0.));
#40044=CARTESIAN_POINT('',(40.9702,2.41935000000001,-2.96284923351715E-16));
#40045=CARTESIAN_POINT('',(40.9702,2.41935000000001,-2.96284923351715E-16));
#40046=CARTESIAN_POINT('',(40.9702,-2.41935,3.42023499377406E-16));
#40047=CARTESIAN_POINT('Origin',(40.9702,3.22869914397977E-15,0.));
#40048=CARTESIAN_POINT('Origin',(40.9702,3.22869914397977E-15,0.));
#40049=CARTESIAN_POINT('Origin',(41.4993118262482,3.29349451441038E-15,
0.));
#40050=CARTESIAN_POINT('',(41.4993118262482,-3.175,-3.88825358729285E-16));
#40051=CARTESIAN_POINT('Origin',(0.,0.,0.));
#40052=CARTESIAN_POINT('',(40.2293118262482,-3.175,-3.88825358729285E-16));
#40053=CARTESIAN_POINT('',(40.2293118262482,-3.88825358729285E-16,-3.175));
#40054=CARTESIAN_POINT('Origin',(40.2293118262482,3.29349451441038E-15,
0.));
#40055=CARTESIAN_POINT('Origin',(40.2293118262482,3.29349451441038E-15,
0.));
#40056=CARTESIAN_POINT('',(0.,-3.88825358729285E-16,-3.175));
#40057=CARTESIAN_POINT('Origin',(39.7002,3.22869914397977E-15,0.));
#40058=CARTESIAN_POINT('',(39.1710881737518,-3.88825358729285E-16,-3.175));
#40059=CARTESIAN_POINT('',(39.1710881737518,3.17500000000001,-3.88825358729285E-16));
#40060=CARTESIAN_POINT('Origin',(39.1710881737518,3.16390377354917E-15,
0.));
#40061=CARTESIAN_POINT('Origin',(39.1710881737518,3.16390377354917E-15,
0.));
#40062=CARTESIAN_POINT('',(39.7002,2.41935000000001,-2.96284923351715E-16));
#40063=CARTESIAN_POINT('',(39.7002,2.41935000000001,-2.96284923351715E-16));
#40064=CARTESIAN_POINT('',(39.7002,-2.41935,3.425551410405E-16));
#40065=CARTESIAN_POINT('Origin',(39.7002,3.22869914397977E-15,0.));
#40066=CARTESIAN_POINT('Origin',(39.7002,3.22869914397977E-15,0.));
#40067=CARTESIAN_POINT('Origin',(40.2293118262482,3.29349451441038E-15,
0.));
#40068=CARTESIAN_POINT('',(40.2293118262482,-3.175,-3.88825358729285E-16));
#40069=CARTESIAN_POINT('Origin',(0.,0.,0.));
#40070=CARTESIAN_POINT('',(38.9593118262482,-3.175,-3.88825358729285E-16));
#40071=CARTESIAN_POINT('',(38.9593118262482,-3.88825358729285E-16,-3.175));
#40072=CARTESIAN_POINT('Origin',(38.9593118262482,3.29349451441038E-15,
0.));
#40073=CARTESIAN_POINT('Origin',(38.9593118262482,3.29349451441038E-15,
0.));
#40074=CARTESIAN_POINT('',(0.,-3.88825358729285E-16,-3.175));
#40075=CARTESIAN_POINT('Origin',(38.4302,3.22869914397977E-15,0.));
#40076=CARTESIAN_POINT('',(37.9010881737518,-3.88825358729285E-16,-3.175));
#40077=CARTESIAN_POINT('',(37.9010881737518,3.17500000000001,-3.88825358729285E-16));
#40078=CARTESIAN_POINT('Origin',(37.9010881737518,3.16390377354917E-15,
0.));
#40079=CARTESIAN_POINT('Origin',(37.9010881737518,3.16390377354917E-15,
0.));
#40080=CARTESIAN_POINT('',(38.4302,2.41935000000001,-2.96284923351715E-16));
#40081=CARTESIAN_POINT('',(38.4302,2.41935000000001,-2.96284923351715E-16));
#40082=CARTESIAN_POINT('',(38.4302,-2.41935,3.425551410405E-16));
#40083=CARTESIAN_POINT('Origin',(38.4302,3.22869914397977E-15,0.));
#40084=CARTESIAN_POINT('Origin',(38.4302,3.22869914397977E-15,0.));
#40085=CARTESIAN_POINT('Origin',(38.9593118262482,3.29349451441038E-15,
0.));
#40086=CARTESIAN_POINT('',(38.9593118262482,-3.175,-3.88825358729285E-16));
#40087=CARTESIAN_POINT('Origin',(0.,0.,0.));
#40088=CARTESIAN_POINT('',(37.6893118262482,-3.175,-3.88825358729285E-16));
#40089=CARTESIAN_POINT('',(37.6893118262482,-3.88825358729285E-16,-3.175));
#40090=CARTESIAN_POINT('Origin',(37.6893118262482,3.29349451441038E-15,
0.));
#40091=CARTESIAN_POINT('Origin',(37.6893118262482,3.29349451441038E-15,
0.));
#40092=CARTESIAN_POINT('',(0.,-3.88825358729285E-16,-3.175));
#40093=CARTESIAN_POINT('Origin',(37.1602,3.22869914397977E-15,0.));
#40094=CARTESIAN_POINT('',(36.6310881737518,-3.88825358729285E-16,-3.175));
#40095=CARTESIAN_POINT('',(36.6310881737518,3.175,-3.88825358729285E-16));
#40096=CARTESIAN_POINT('Origin',(36.6310881737518,3.16390377354917E-15,
0.));
#40097=CARTESIAN_POINT('Origin',(36.6310881737518,3.16390377354917E-15,
0.));
#40098=CARTESIAN_POINT('',(37.1602,2.41935000000001,-2.96284923351715E-16));
#40099=CARTESIAN_POINT('',(37.1602,2.41935000000001,-2.96284923351715E-16));
#40100=CARTESIAN_POINT('',(37.1602,-2.41935,3.425551410405E-16));
#40101=CARTESIAN_POINT('Origin',(37.1602,3.22869914397977E-15,0.));
#40102=CARTESIAN_POINT('Origin',(37.1602,3.22869914397977E-15,0.));
#40103=CARTESIAN_POINT('Origin',(37.6893118262482,3.29349451441038E-15,
0.));
#40104=CARTESIAN_POINT('',(37.6893118262482,-3.175,-3.88825358729285E-16));
#40105=CARTESIAN_POINT('Origin',(0.,0.,0.));
#40106=CARTESIAN_POINT('',(36.4193118262482,-3.175,-3.88825358729285E-16));
#40107=CARTESIAN_POINT('',(36.4193118262482,-3.88825358729285E-16,-3.175));
#40108=CARTESIAN_POINT('Origin',(36.4193118262482,3.29349451441038E-15,
0.));
#40109=CARTESIAN_POINT('Origin',(36.4193118262482,3.29349451441038E-15,
0.));
#40110=CARTESIAN_POINT('',(0.,-3.88825358729285E-16,-3.175));
#40111=CARTESIAN_POINT('Origin',(35.8902,3.22869914397977E-15,0.));
#40112=CARTESIAN_POINT('',(35.3610881737518,-3.88825358729285E-16,-3.175));
#40113=CARTESIAN_POINT('',(35.3610881737518,3.17500000000001,-3.88825358729285E-16));
#40114=CARTESIAN_POINT('Origin',(35.3610881737518,3.16390377354917E-15,
0.));
#40115=CARTESIAN_POINT('Origin',(35.3610881737518,3.16390377354917E-15,
0.));
#40116=CARTESIAN_POINT('',(35.8902,2.41935000000001,-2.96284923351715E-16));
#40117=CARTESIAN_POINT('',(35.8902,2.41935000000001,-2.96284923351715E-16));
#40118=CARTESIAN_POINT('',(35.8902,-2.41935,3.425551410405E-16));
#40119=CARTESIAN_POINT('Origin',(35.8902,3.22869914397977E-15,0.));
#40120=CARTESIAN_POINT('Origin',(35.8902,3.22869914397977E-15,0.));
#40121=CARTESIAN_POINT('Origin',(36.4193118262482,3.29349451441038E-15,
0.));
#40122=CARTESIAN_POINT('',(36.4193118262482,-3.175,-3.88825358729285E-16));
#40123=CARTESIAN_POINT('Origin',(0.,0.,0.));
#40124=CARTESIAN_POINT('',(35.1493118262482,-3.175,-3.88825358729285E-16));
#40125=CARTESIAN_POINT('',(35.1493118262482,-3.88825358729285E-16,-3.175));
#40126=CARTESIAN_POINT('Origin',(35.1493118262482,3.29349451441038E-15,
0.));
#40127=CARTESIAN_POINT('Origin',(35.1493118262482,3.29349451441038E-15,
0.));
#40128=CARTESIAN_POINT('',(0.,-3.88825358729285E-16,-3.175));
#40129=CARTESIAN_POINT('Origin',(34.6202,3.22869914397977E-15,0.));
#40130=CARTESIAN_POINT('',(34.0910881737518,-3.88825358729285E-16,-3.175));
#40131=CARTESIAN_POINT('',(34.0910881737518,3.17500000000001,-3.88825358729285E-16));
#40132=CARTESIAN_POINT('Origin',(34.0910881737518,3.16390377354917E-15,
0.));
#40133=CARTESIAN_POINT('Origin',(34.0910881737518,3.16390377354917E-15,
0.));
#40134=CARTESIAN_POINT('',(34.6202,2.41935000000001,-2.96284923351715E-16));
#40135=CARTESIAN_POINT('',(34.6202,2.41935000000001,-2.96284923351715E-16));
#40136=CARTESIAN_POINT('',(34.6202,-2.41935,3.425551410405E-16));
#40137=CARTESIAN_POINT('Origin',(34.6202,3.22869914397977E-15,0.));
#40138=CARTESIAN_POINT('Origin',(34.6202,3.22869914397977E-15,0.));
#40139=CARTESIAN_POINT('Origin',(35.1493118262482,3.29349451441038E-15,
0.));
#40140=CARTESIAN_POINT('',(35.1493118262482,-3.175,-3.88825358729285E-16));
#40141=CARTESIAN_POINT('Origin',(0.,0.,0.));
#40142=CARTESIAN_POINT('',(33.8793118262482,-3.175,-3.88825358729285E-16));
#40143=CARTESIAN_POINT('',(33.8793118262482,-3.88825358729285E-16,-3.175));
#40144=CARTESIAN_POINT('Origin',(33.8793118262482,3.29349451441038E-15,
0.));
#40145=CARTESIAN_POINT('Origin',(33.8793118262482,3.29349451441038E-15,
0.));
#40146=CARTESIAN_POINT('',(0.,-3.88825358729285E-16,-3.175));
#40147=CARTESIAN_POINT('Origin',(33.3502,3.22869914397977E-15,0.));
#40148=CARTESIAN_POINT('',(32.8210881737518,-3.88825358729285E-16,-3.175));
#40149=CARTESIAN_POINT('',(32.8210881737518,3.175,-3.88825358729285E-16));
#40150=CARTESIAN_POINT('Origin',(32.8210881737518,3.16390377354917E-15,
0.));
#40151=CARTESIAN_POINT('Origin',(32.8210881737518,3.16390377354917E-15,
0.));
#40152=CARTESIAN_POINT('',(33.3502,2.41935000000001,-2.96284923351715E-16));
#40153=CARTESIAN_POINT('',(33.3502,2.41935000000001,-2.96284923351715E-16));
#40154=CARTESIAN_POINT('',(33.3502,-2.41935,3.425551410405E-16));
#40155=CARTESIAN_POINT('Origin',(33.3502,3.22869914397977E-15,0.));
#40156=CARTESIAN_POINT('Origin',(33.3502,3.22869914397977E-15,0.));
#40157=CARTESIAN_POINT('Origin',(33.8793118262482,3.29349451441038E-15,
0.));
#40158=CARTESIAN_POINT('',(33.8793118262482,-3.175,-3.88825358729285E-16));
#40159=CARTESIAN_POINT('Origin',(0.,0.,0.));
#40160=CARTESIAN_POINT('',(32.6093118262482,-3.175,-3.88825358729285E-16));
#40161=CARTESIAN_POINT('',(32.6093118262482,-3.88825358729285E-16,-3.175));
#40162=CARTESIAN_POINT('Origin',(32.6093118262482,3.29349451441038E-15,
0.));
#40163=CARTESIAN_POINT('Origin',(32.6093118262482,3.29349451441038E-15,
0.));
#40164=CARTESIAN_POINT('',(0.,-3.88825358729285E-16,-3.175));
#40165=CARTESIAN_POINT('Origin',(32.0802,3.22869914397977E-15,0.));
#40166=CARTESIAN_POINT('',(31.5510881737518,-3.88825358729285E-16,-3.175));
#40167=CARTESIAN_POINT('',(31.5510881737518,3.17500000000001,-3.88825358729285E-16));
#40168=CARTESIAN_POINT('Origin',(31.5510881737518,3.16390377354917E-15,
0.));
#40169=CARTESIAN_POINT('Origin',(31.5510881737518,3.16390377354917E-15,
0.));
#40170=CARTESIAN_POINT('',(32.0802,2.41935000000001,-2.96284923351715E-16));
#40171=CARTESIAN_POINT('',(32.0802,2.41935000000001,-2.96284923351715E-16));
#40172=CARTESIAN_POINT('',(32.0802,-2.41935,3.425551410405E-16));
#40173=CARTESIAN_POINT('Origin',(32.0802,3.22869914397977E-15,0.));
#40174=CARTESIAN_POINT('Origin',(32.0802,3.22869914397977E-15,0.));
#40175=CARTESIAN_POINT('Origin',(32.6093118262482,3.29349451441038E-15,
0.));
#40176=CARTESIAN_POINT('',(32.6093118262482,-3.175,-3.88825358729285E-16));
#40177=CARTESIAN_POINT('Origin',(0.,0.,0.));
#40178=CARTESIAN_POINT('',(31.3393118262482,-3.175,-3.88825358729285E-16));
#40179=CARTESIAN_POINT('',(31.3393118262482,-3.88825358729285E-16,-3.175));
#40180=CARTESIAN_POINT('Origin',(31.3393118262482,3.29349451441038E-15,
0.));
#40181=CARTESIAN_POINT('Origin',(31.3393118262482,3.29349451441038E-15,
0.));
#40182=CARTESIAN_POINT('',(0.,-3.88825358729285E-16,-3.175));
#40183=CARTESIAN_POINT('Origin',(30.8102,3.22869914397977E-15,0.));
#40184=CARTESIAN_POINT('',(30.2810881737518,-3.88825358729285E-16,-3.175));
#40185=CARTESIAN_POINT('',(30.2810881737518,3.17500000000001,-3.88825358729285E-16));
#40186=CARTESIAN_POINT('Origin',(30.2810881737518,3.16390377354917E-15,
0.));
#40187=CARTESIAN_POINT('Origin',(30.2810881737518,3.16390377354917E-15,
0.));
#40188=CARTESIAN_POINT('',(30.8102,2.41935000000001,-2.96284923351715E-16));
#40189=CARTESIAN_POINT('',(30.8102,2.41935000000001,-2.96284923351715E-16));
#40190=CARTESIAN_POINT('',(30.8102,-2.41935,3.425551410405E-16));
#40191=CARTESIAN_POINT('Origin',(30.8102,3.22869914397977E-15,0.));
#40192=CARTESIAN_POINT('Origin',(30.8102,3.22869914397977E-15,0.));
#40193=CARTESIAN_POINT('Origin',(31.3393118262482,3.29349451441038E-15,
0.));
#40194=CARTESIAN_POINT('',(31.3393118262482,-3.175,-3.88825358729285E-16));
#40195=CARTESIAN_POINT('Origin',(0.,0.,0.));
#40196=CARTESIAN_POINT('',(30.0693118262482,-3.175,-3.88825358729285E-16));
#40197=CARTESIAN_POINT('',(30.0693118262482,-3.88825358729285E-16,-3.175));
#40198=CARTESIAN_POINT('Origin',(30.0693118262482,3.29349451441038E-15,
0.));
#40199=CARTESIAN_POINT('Origin',(30.0693118262482,3.29349451441038E-15,
0.));
#40200=CARTESIAN_POINT('',(0.,-3.88825358729285E-16,-3.175));
#40201=CARTESIAN_POINT('Origin',(29.5402,3.22869914397977E-15,0.));
#40202=CARTESIAN_POINT('',(29.0110881737518,-3.88825358729285E-16,-3.175));
#40203=CARTESIAN_POINT('',(29.0110881737518,3.17500000000001,-3.88825358729285E-16));
#40204=CARTESIAN_POINT('Origin',(29.0110881737518,3.16390377354917E-15,
0.));
#40205=CARTESIAN_POINT('Origin',(29.0110881737518,3.16390377354917E-15,
0.));
#40206=CARTESIAN_POINT('',(29.5402,2.41935000000001,-2.96284923351715E-16));
#40207=CARTESIAN_POINT('',(29.5402,2.41935000000001,-2.96284923351715E-16));
#40208=CARTESIAN_POINT('',(29.5402,-2.41935,3.425551410405E-16));
#40209=CARTESIAN_POINT('Origin',(29.5402,3.22869914397977E-15,0.));
#40210=CARTESIAN_POINT('Origin',(29.5402,3.22869914397977E-15,0.));
#40211=CARTESIAN_POINT('Origin',(30.0693118262482,3.29349451441038E-15,
0.));
#40212=CARTESIAN_POINT('',(30.0693118262482,-3.175,-3.88825358729285E-16));
#40213=CARTESIAN_POINT('Origin',(0.,0.,0.));
#40214=CARTESIAN_POINT('',(28.7993118262482,-3.175,-3.88825358729285E-16));
#40215=CARTESIAN_POINT('',(28.7993118262482,-3.88825358729285E-16,-3.175));
#40216=CARTESIAN_POINT('Origin',(28.7993118262482,3.29349451441038E-15,
0.));
#40217=CARTESIAN_POINT('Origin',(28.7993118262482,3.29349451441038E-15,
0.));
#40218=CARTESIAN_POINT('',(0.,-3.88825358729285E-16,-3.175));
#40219=CARTESIAN_POINT('Origin',(28.2702,3.22869914397977E-15,0.));
#40220=CARTESIAN_POINT('',(27.7410881737518,-3.88825358729285E-16,-3.175));
#40221=CARTESIAN_POINT('',(27.7410881737518,3.17500000000001,-3.88825358729285E-16));
#40222=CARTESIAN_POINT('Origin',(27.7410881737518,3.16390377354917E-15,
0.));
#40223=CARTESIAN_POINT('Origin',(27.7410881737518,3.16390377354917E-15,
0.));
#40224=CARTESIAN_POINT('',(28.2702,2.41935000000001,-2.96284923351715E-16));
#40225=CARTESIAN_POINT('',(28.2702,2.41935000000001,-2.96284923351715E-16));
#40226=CARTESIAN_POINT('',(28.2702,-2.41935,3.425551410405E-16));
#40227=CARTESIAN_POINT('Origin',(28.2702,3.22869914397977E-15,0.));
#40228=CARTESIAN_POINT('Origin',(28.2702,3.22869914397977E-15,0.));
#40229=CARTESIAN_POINT('Origin',(28.7993118262482,3.29349451441038E-15,
0.));
#40230=CARTESIAN_POINT('',(28.7993118262482,-3.175,-3.88825358729285E-16));
#40231=CARTESIAN_POINT('Origin',(0.,0.,0.));
#40232=CARTESIAN_POINT('',(27.5293118262482,-3.175,-3.88825358729285E-16));
#40233=CARTESIAN_POINT('',(27.5293118262482,-3.88825358729285E-16,-3.175));
#40234=CARTESIAN_POINT('Origin',(27.5293118262482,3.29349451441038E-15,
0.));
#40235=CARTESIAN_POINT('Origin',(27.5293118262482,3.29349451441038E-15,
0.));
#40236=CARTESIAN_POINT('',(0.,-3.88825358729285E-16,-3.175));
#40237=CARTESIAN_POINT('Origin',(27.0002,3.22869914397977E-15,0.));
#40238=CARTESIAN_POINT('',(26.4710881737518,-3.88825358729285E-16,-3.175));
#40239=CARTESIAN_POINT('',(26.4710881737518,3.17500000000001,-3.88825358729285E-16));
#40240=CARTESIAN_POINT('Origin',(26.4710881737518,3.16390377354917E-15,
0.));
#40241=CARTESIAN_POINT('Origin',(26.4710881737518,3.16390377354917E-15,
0.));
#40242=CARTESIAN_POINT('',(27.0002,2.41935000000001,-2.96284923351715E-16));
#40243=CARTESIAN_POINT('',(27.0002,2.41935000000001,-2.96284923351715E-16));
#40244=CARTESIAN_POINT('',(27.0002,-2.41935,3.425551410405E-16));
#40245=CARTESIAN_POINT('Origin',(27.0002,3.22869914397977E-15,0.));
#40246=CARTESIAN_POINT('Origin',(27.0002,3.22869914397977E-15,0.));
#40247=CARTESIAN_POINT('Origin',(27.5293118262482,3.29349451441038E-15,
0.));
#40248=CARTESIAN_POINT('',(27.5293118262482,-3.175,-3.88825358729285E-16));
#40249=CARTESIAN_POINT('Origin',(0.,0.,0.));
#40250=CARTESIAN_POINT('',(26.2593118262482,-3.175,-3.88825358729285E-16));
#40251=CARTESIAN_POINT('',(26.2593118262482,-3.88825358729285E-16,-3.175));
#40252=CARTESIAN_POINT('Origin',(26.2593118262482,3.29349451441038E-15,
0.));
#40253=CARTESIAN_POINT('Origin',(26.2593118262482,3.29349451441038E-15,
0.));
#40254=CARTESIAN_POINT('',(0.,-3.88825358729285E-16,-3.175));
#40255=CARTESIAN_POINT('Origin',(25.7302,3.22869914397977E-15,0.));
#40256=CARTESIAN_POINT('',(25.2010881737518,-3.88825358729285E-16,-3.175));
#40257=CARTESIAN_POINT('',(25.2010881737518,3.17500000000001,-3.88825358729285E-16));
#40258=CARTESIAN_POINT('Origin',(25.2010881737518,3.16390377354917E-15,
0.));
#40259=CARTESIAN_POINT('Origin',(25.2010881737518,3.16390377354917E-15,
0.));
#40260=CARTESIAN_POINT('',(25.7302,2.41935000000001,-2.96284923351715E-16));
#40261=CARTESIAN_POINT('',(25.7302,2.41935000000001,-2.96284923351715E-16));
#40262=CARTESIAN_POINT('',(25.7302,-2.41935,3.425551410405E-16));
#40263=CARTESIAN_POINT('Origin',(25.7302,3.22869914397977E-15,0.));
#40264=CARTESIAN_POINT('Origin',(25.7302,3.22869914397977E-15,0.));
#40265=CARTESIAN_POINT('Origin',(26.2593118262482,3.29349451441038E-15,
0.));
#40266=CARTESIAN_POINT('',(26.2593118262482,-3.175,-3.88825358729285E-16));
#40267=CARTESIAN_POINT('Origin',(0.,0.,0.));
#40268=CARTESIAN_POINT('',(24.9893118262482,-3.175,-3.88825358729285E-16));
#40269=CARTESIAN_POINT('',(24.9893118262482,-3.88825358729285E-16,-3.175));
#40270=CARTESIAN_POINT('Origin',(24.9893118262482,3.29349451441038E-15,
0.));
#40271=CARTESIAN_POINT('Origin',(24.9893118262482,3.29349451441038E-15,
0.));
#40272=CARTESIAN_POINT('',(0.,-3.88825358729285E-16,-3.175));
#40273=CARTESIAN_POINT('Origin',(24.4602,3.22869914397977E-15,0.));
#40274=CARTESIAN_POINT('',(23.9310881737518,-3.88825358729285E-16,-3.175));
#40275=CARTESIAN_POINT('',(23.9310881737518,3.17500000000001,-3.88825358729285E-16));
#40276=CARTESIAN_POINT('Origin',(23.9310881737518,3.16390377354917E-15,
0.));
#40277=CARTESIAN_POINT('Origin',(23.9310881737518,3.16390377354917E-15,
0.));
#40278=CARTESIAN_POINT('',(24.4602,2.41935000000001,-2.96284923351715E-16));
#40279=CARTESIAN_POINT('',(24.4602,2.41935000000001,-2.96284923351715E-16));
#40280=CARTESIAN_POINT('',(24.4602,-2.41935,3.425551410405E-16));
#40281=CARTESIAN_POINT('Origin',(24.4602,3.22869914397977E-15,0.));
#40282=CARTESIAN_POINT('Origin',(24.4602,3.22869914397977E-15,0.));
#40283=CARTESIAN_POINT('Origin',(24.9893118262482,3.29349451441038E-15,
0.));
#40284=CARTESIAN_POINT('',(24.9893118262482,-3.175,-3.88825358729285E-16));
#40285=CARTESIAN_POINT('Origin',(0.,0.,0.));
#40286=CARTESIAN_POINT('',(23.7193118262482,-3.175,-3.88825358729285E-16));
#40287=CARTESIAN_POINT('',(23.7193118262482,-3.88825358729285E-16,-3.175));
#40288=CARTESIAN_POINT('Origin',(23.7193118262482,3.29349451441038E-15,
0.));
#40289=CARTESIAN_POINT('Origin',(23.7193118262482,3.29349451441038E-15,
0.));
#40290=CARTESIAN_POINT('',(0.,-3.88825358729285E-16,-3.175));
#40291=CARTESIAN_POINT('Origin',(23.1902,3.22869914397977E-15,0.));
#40292=CARTESIAN_POINT('',(22.6610881737518,-3.88825358729285E-16,-3.175));
#40293=CARTESIAN_POINT('',(22.6610881737518,3.17500000000001,-3.88825358729285E-16));
#40294=CARTESIAN_POINT('Origin',(22.6610881737518,3.16390377354917E-15,
0.));
#40295=CARTESIAN_POINT('Origin',(22.6610881737518,3.16390377354917E-15,
0.));
#40296=CARTESIAN_POINT('',(23.1902,2.41935000000001,-2.96284923351715E-16));
#40297=CARTESIAN_POINT('',(23.1902,2.41935000000001,-2.96284923351715E-16));
#40298=CARTESIAN_POINT('',(23.1902,-2.41935,3.425551410405E-16));
#40299=CARTESIAN_POINT('Origin',(23.1902,3.22869914397977E-15,0.));
#40300=CARTESIAN_POINT('Origin',(23.1902,3.22869914397977E-15,0.));
#40301=CARTESIAN_POINT('Origin',(23.7193118262482,3.29349451441038E-15,
0.));
#40302=CARTESIAN_POINT('',(23.7193118262482,-3.175,-3.88825358729285E-16));
#40303=CARTESIAN_POINT('Origin',(4.5212,0.,0.));
#40304=CARTESIAN_POINT('',(4.5212,3.88825358729285E-16,-3.175));
#40305=CARTESIAN_POINT('',(4.5212,-3.88825358729285E-16,3.175));
#40306=CARTESIAN_POINT('Origin',(4.5212,0.,0.));
#40307=CARTESIAN_POINT('Origin',(4.5212,0.,0.));
#40308=CARTESIAN_POINT('',(4.1402,-4.35484401776799E-16,3.556));
#40309=CARTESIAN_POINT('Origin',(4.5212,-4.35484401776799E-16,3.556));
#40310=CARTESIAN_POINT('Origin',(4.1402,0.,0.));
#40311=CARTESIAN_POINT('Origin',(0.,0.,0.));
#40312=CARTESIAN_POINT('',(3.7592,-4.81735291109131,2.78130000000001));
#40313=CARTESIAN_POINT('',(3.7592,0.,5.5626));
#40314=CARTESIAN_POINT('Origin',(3.7592,0.,0.));
#40315=CARTESIAN_POINT('',(3.7592,-4.81735291109132,-2.7813));
#40316=CARTESIAN_POINT('Origin',(3.7592,0.,0.));
#40317=CARTESIAN_POINT('',(3.7592,7.5115729936858E-16,-5.5626));
#40318=CARTESIAN_POINT('Origin',(3.7592,0.,0.));
#40319=CARTESIAN_POINT('',(4.1402,-6.81222028493707E-16,-5.5626));
#40320=CARTESIAN_POINT('',(0.,-6.81222028493707E-16,-5.5626));
#40321=CARTESIAN_POINT('Origin',(4.1402,0.,0.));
#40322=CARTESIAN_POINT('',(3.7592,4.81735291109132,-2.78130000000001));
#40323=CARTESIAN_POINT('Origin',(3.7592,0.,0.));
#40324=CARTESIAN_POINT('',(3.7592,4.81735291109131,2.78130000000001));
#40325=CARTESIAN_POINT('Origin',(3.7592,0.,0.));
#40326=CARTESIAN_POINT('Origin',(3.7592,0.,0.));
#40327=CARTESIAN_POINT('Origin',(0.,0.,0.));
#40328=CARTESIAN_POINT('',(0.,-3.88825358729285E-16,-3.175));
#40329=CARTESIAN_POINT('Origin',(4.1402,6.42313721478843,1.3010426069826E-15));
#40330=CARTESIAN_POINT('Origin',(3.7592,5.5626,0.));
#40331=CARTESIAN_POINT('',(3.7592,3.21156860739421,-5.5626));
#40332=CARTESIAN_POINT('',(3.7592,3.21156860739421,-5.5626));
#40333=CARTESIAN_POINT('',(3.7592,3.21156860739421,-5.5626));
#40334=CARTESIAN_POINT('Origin',(3.7592,5.5626,0.));
#40335=CARTESIAN_POINT('',(3.7592,6.42313721478843,0.));
#40336=CARTESIAN_POINT('',(3.7592,3.21156860739421,-5.5626));
#40337=CARTESIAN_POINT('',(3.7592,6.42313721478843,0.));
#40338=CARTESIAN_POINT('Origin',(3.7592,5.5626,0.));
#40339=CARTESIAN_POINT('',(3.7592,3.21156860739421,5.5626));
#40340=CARTESIAN_POINT('',(3.7592,6.42313721478843,0.));
#40341=CARTESIAN_POINT('',(3.7592,3.21156860739421,5.5626));
#40342=CARTESIAN_POINT('Origin',(3.7592,5.5626,0.));
#40343=CARTESIAN_POINT('',(3.7592,-3.21156860739419,5.5626));
#40344=CARTESIAN_POINT('',(3.7592,3.21156860739421,5.5626));
#40345=CARTESIAN_POINT('',(3.7592,-6.42313721478842,0.));
#40346=CARTESIAN_POINT('Origin',(3.7592,5.5626,0.));
#40347=CARTESIAN_POINT('',(3.7592,-6.42313721478842,-8.67361737988404E-16));
#40348=CARTESIAN_POINT('',(3.7592,-6.42313721478842,0.));
#40349=CARTESIAN_POINT('',(3.7592,-3.21156860739422,-5.5626));
#40350=CARTESIAN_POINT('Origin',(3.7592,5.5626,0.));
#40351=CARTESIAN_POINT('',(3.7592,-3.21156860739422,-5.5626));
#40352=CARTESIAN_POINT('',(3.7592,-3.21156860739422,-5.5626));
#40353=CARTESIAN_POINT('',(3.7592,3.21156860739421,-5.5626));
#40354=CARTESIAN_POINT('Origin',(0.,6.42313721478843,1.3010426069826E-15));
#40355=CARTESIAN_POINT('',(0.,7.5115729936858E-16,-5.5626));
#40356=CARTESIAN_POINT('',(0.,4.81735291109131,-2.78130000000001));
#40357=CARTESIAN_POINT('Origin',(0.,0.,0.));
#40358=CARTESIAN_POINT('',(0.,-4.81735291109132,-2.7813));
#40359=CARTESIAN_POINT('Origin',(0.,0.,0.));
#40360=CARTESIAN_POINT('',(0.,-4.81735291109131,2.78130000000001));
#40361=CARTESIAN_POINT('Origin',(0.,0.,0.));
#40362=CARTESIAN_POINT('',(0.,7.51157299368582E-16,5.5626));
#40363=CARTESIAN_POINT('Origin',(0.,0.,0.));
#40364=CARTESIAN_POINT('',(0.,4.81735291109131,2.78130000000001));
#40365=CARTESIAN_POINT('Origin',(0.,0.,0.));
#40366=CARTESIAN_POINT('Origin',(0.,0.,0.));
#40367=CARTESIAN_POINT('Origin',(0.,0.,0.));
#40368=CARTESIAN_POINT('',(0.496831392605788,6.42313721478843,3.39052593516398E-16));
#40369=CARTESIAN_POINT('Ctrl Pts',(0.,4.81735291109132,2.78130000000001));
#40370=CARTESIAN_POINT('Ctrl Pts',(1.11022302462516E-16,5.56260000000048,
1.49049417781655));
#40371=CARTESIAN_POINT('Ctrl Pts',(0.496831392606468,6.42313721478961,-2.03913353027845E-12));
#40372=CARTESIAN_POINT('Ctrl Pts',(0.496831392606465,6.4231372147896,2.03638537188185E-12));
#40373=CARTESIAN_POINT('Ctrl Pts',(-2.59160509497383E-15,5.56260000000047,
-1.49049417781655));
#40374=CARTESIAN_POINT('Ctrl Pts',(-1.14788227546538E-15,4.81735291109131,
-2.78130000000001));
#40375=CARTESIAN_POINT('Origin',(0.,0.,0.));
#40376=CARTESIAN_POINT('',(0.496831392605783,3.21156860739421,5.5626));
#40377=CARTESIAN_POINT('Ctrl Pts',(-2.55084950103419E-16,-3.06101940124103E-15,
5.5626));
#40378=CARTESIAN_POINT('Ctrl Pts',(-8.88178419700125E-16,1.49049417781831,
5.5626));
#40379=CARTESIAN_POINT('Ctrl Pts',(0.496831392606465,3.21156860739657,5.5626));
#40380=CARTESIAN_POINT('Ctrl Pts',(0.496831392606461,3.21156860739304,5.56260000000203));
#40381=CARTESIAN_POINT('Ctrl Pts',(0.,4.07210582218216,4.07210582218346));
#40382=CARTESIAN_POINT('Ctrl Pts',(0.,4.81735291109132,2.78130000000001));
#40383=CARTESIAN_POINT('Origin',(0.,0.,0.));
#40384=CARTESIAN_POINT('',(0.496831392605779,-3.21156860739419,5.5626));
#40385=CARTESIAN_POINT('Ctrl Pts',(0.496831392606463,-3.21156860739656,
5.5626));
#40386=CARTESIAN_POINT('Ctrl Pts',(1.23283174735618E-16,-1.49049417781831,
5.5626));
#40387=CARTESIAN_POINT('Ctrl Pts',(-2.55084950103419E-16,-3.06101940124103E-15,
5.5626));
#40388=CARTESIAN_POINT('Ctrl Pts',(-6.24958127753376E-15,-4.81735291109131,
2.7813));
#40389=CARTESIAN_POINT('Ctrl Pts',(-6.82787160144471E-15,-4.07210582218215,
4.07210582218346));
#40390=CARTESIAN_POINT('Ctrl Pts',(0.496831392606459,-3.21156860739302,
5.56260000000204));
#40391=CARTESIAN_POINT('Origin',(0.,0.,0.));
#40392=CARTESIAN_POINT('',(0.496831392605783,-6.42313721478842,3.05208903104958E-16));
#40393=CARTESIAN_POINT('Ctrl Pts',(0.496831392606464,-6.4231372147896,-2.04160687283539E-12));
#40394=CARTESIAN_POINT('Ctrl Pts',(-5.87150394869329E-15,-5.56260000000047,
1.49049417781655));
#40395=CARTESIAN_POINT('Ctrl Pts',(-6.24958127753376E-15,-4.81735291109131,
2.7813));
#40396=CARTESIAN_POINT('Ctrl Pts',(1.40296722556881E-15,-4.81735291109132,
-2.7813));
#40397=CARTESIAN_POINT('Ctrl Pts',(1.38777878078145E-15,-5.56260000000048,
-1.49049417781654));
#40398=CARTESIAN_POINT('Ctrl Pts',(0.496831392606464,-6.4231372147896,2.03720981940083E-12));
#40399=CARTESIAN_POINT('Origin',(0.,0.,0.));
#40400=CARTESIAN_POINT('',(0.496831392605783,3.21156860739421,-5.5626));
#40401=CARTESIAN_POINT('Ctrl Pts',(-1.14788227546538E-15,4.81735291109131,
-2.78130000000001));
#40402=CARTESIAN_POINT('Ctrl Pts',(4.44089209850063E-16,4.07210582218215,
-4.07210582218347));
#40403=CARTESIAN_POINT('Ctrl Pts',(0.496831392606464,3.21156860739303,-5.56260000000204));
#40404=CARTESIAN_POINT('Ctrl Pts',(0.496831392606462,3.21156860739656,-5.5626));
#40405=CARTESIAN_POINT('Ctrl Pts',(-4.83028869377251E-16,1.49049417781831,
-5.5626));
#40406=CARTESIAN_POINT('Ctrl Pts',(-5.10169900206839E-16,0.,-5.5626));
#40407=CARTESIAN_POINT('Origin',(0.,0.,0.));
#40408=CARTESIAN_POINT('',(0.496831392605573,-3.21156860739453,-5.5626));
#40409=CARTESIAN_POINT('Ctrl Pts',(0.49683139260641,-3.21156860739314,-5.56260000000187));
#40410=CARTESIAN_POINT('Ctrl Pts',(1.46512849432153E-15,-4.07210582218221,
-4.07210582218339));
#40411=CARTESIAN_POINT('Ctrl Pts',(1.40296722556881E-15,-4.81735291109132,
-2.7813));
#40412=CARTESIAN_POINT('Ctrl Pts',(-5.10169900206839E-16,0.,-5.5626));
#40413=CARTESIAN_POINT('Ctrl Pts',(-3.33066907387547E-16,-1.49049417781841,
-5.5626));
#40414=CARTESIAN_POINT('Ctrl Pts',(0.496831392606533,-3.21156860739681,
-5.5626));
#40415=CARTESIAN_POINT('Origin',(4.1402,3.21156860739421,-5.5626));
#40416=CARTESIAN_POINT('',(4.1402,-3.21156860739422,-5.5626));
#40417=CARTESIAN_POINT('',(4.1402,3.21156860739421,-5.5626));
#40418=CARTESIAN_POINT('Origin',(4.1402,-3.21156860739422,-5.5626));
#40419=CARTESIAN_POINT('',(4.1402,-6.42313721478842,0.));
#40420=CARTESIAN_POINT('Origin',(4.1402,-6.42313721478842,0.));
#40421=CARTESIAN_POINT('',(4.1402,-3.21156860739419,5.5626));
#40422=CARTESIAN_POINT('Origin',(4.1402,3.21156860739421,5.5626));
#40423=CARTESIAN_POINT('',(4.1402,3.21156860739421,5.5626));
#40424=CARTESIAN_POINT('Origin',(4.1402,6.42313721478843,0.));
#40425=CARTESIAN_POINT('',(4.1402,6.42313721478843,0.));
#40426=CARTESIAN_POINT('Origin',(4.1402,3.21156860739421,-5.5626));
#40427=CARTESIAN_POINT('Origin',(42.2402,0.,0.));
#40796=UNCERTAINTY_MEASURE_WITH_UNIT(LENGTH_MEASURE(0.01),#40810,
'DISTANCE_ACCURACY_VALUE',
'Maximum model space distance between geometric entities at asserted c
onnectivities');
#40799=UNCERTAINTY_MEASURE_WITH_UNIT(LENGTH_MEASURE(0.01),#40810,
'DISTANCE_ACCURACY_VALUE',
'Maximum model space distance between geometric entities at asserted c
onnectivities');
#40806=(
GEOMETRIC_REPRESENTATION_CONTEXT(3)
GLOBAL_UNCERTAINTY_ASSIGNED_CONTEXT((#40796))
GLOBAL_UNIT_ASSIGNED_CONTEXT((#40810,#40812,#40813))
REPRESENTATION_CONTEXT('','3D')
);
#40809=(
GEOMETRIC_REPRESENTATION_CONTEXT(3)
GLOBAL_UNCERTAINTY_ASSIGNED_CONTEXT((#40799))
GLOBAL_UNIT_ASSIGNED_CONTEXT((#40810,#40812,#40813))
REPRESENTATION_CONTEXT('','3D')
);
#40810=(
LENGTH_UNIT()
NAMED_UNIT(*)
SI_UNIT(.MILLI.,.METRE.)
);
#40812=(
NAMED_UNIT(*)
PLANE_ANGLE_UNIT()
SI_UNIT($,.RADIAN.)
);
#40813=(
NAMED_UNIT(*)
SI_UNIT($,.STERADIAN.)
SOLID_ANGLE_UNIT()
);
#40820=SHAPE_DEFINITION_REPRESENTATION(#40829,#40862);
#40829=PRODUCT_DEFINITION_SHAPE('',$,#40872);
#40862=SHAPE_REPRESENTATION('',(#6836),#40806);
#40865=PRODUCT_DEFINITION_CONTEXT('part definition',#40894,'design');
#40872=PRODUCT_DEFINITION('Hex Finished Bolt 0.25-20x1.5x0.75-S',
'Hex Finished Bolt 0.25-20x1.5x0.75-S',#40881,#40865);
#40881=PRODUCT_DEFINITION_FORMATION('',$,#40902);
#40894=APPLICATION_CONTEXT(
'Core Data for Automotive Mechanical Design Process');
#40895=PRODUCT_CONTEXT('part definition',#40894,'mechanical');
#40902=PRODUCT('Hex Finished Bolt 0.25-20x1.5x0.75-S',
'Hex Finished Bolt 0.25-20x1.5x0.75-S',$,(#40895));
#40909=PRESENTATION_STYLE_ASSIGNMENT((#40914));
#40914=SURFACE_STYLE_USAGE(.BOTH.,#40919);
#40919=SURFACE_SIDE_STYLE('',(#40924));
#40924=SURFACE_STYLE_FILL_AREA(#40929);
#40929=FILL_AREA_STYLE('Opaque(31,36,43)',(#40934));
#40934=FILL_AREA_STYLE_COLOUR('Opaque(31,36,43)',#40939);
#40939=COLOUR_RGB('Opaque(31,36,43)',0.12156862745098,0.141176470588235,
0.168627450980392);
ENDSEC;
END-ISO-10303-21;
